ISO-10303-21;
HEADER;
FILE_DESCRIPTION (('STEP AP214'),
    '1' );
FILE_NAME ('instrument roller bearing_iso_ISO 1224 - 180816 - R,14,SI,NC,14.step',
    '2026-09-28T15:49:00',
    ( '' ),
    ( '' ),
    'SwSTEP 2.0',
    'SolidWorks 2026',
    '' );
FILE_SCHEMA (( 'AUTOMOTIVE_DESIGN' ));
ENDSEC;

DATA;
#97=AXIS2_PLACEMENT_3D ( 'NONE', #12823, #1667, #2025 ) ;
#162=EDGE_LOOP ( 'NONE', ( #12105, #9700 ) ) ;
#183=CARTESIAN_POINT ( 'NONE',  ( -90.00000000000002842, 0.000000000000000000, 6.938893903907228378E-15 ) ) ;
#188=EDGE_CURVE ( 'NONE', #23209, #29518, #12364, .T. ) ;
#270=AXIS2_PLACEMENT_3D ( 'NONE', #1715, #16715, #22475 ) ;
#332=DIRECTION ( 'NONE',  ( 1.000000000000000000, -5.339440136655842133E-16, -1.047965281155519420E-16 ) ) ;
#350=CIRCLE ( 'NONE', #918, 6.984000000000015085 ) ;
#354=CARTESIAN_POINT ( 'NONE',  ( 2.000000000000001776, 0.000000000000000000, 0.000000000000000000 ) ) ;
#431=EDGE_CURVE ( 'NONE', #31128, #23989, #2442, .T. ) ;
#435=EDGE_CURVE ( 'NONE', #31128, #24732, #16826, .T. ) ;
#463=EDGE_CURVE ( 'NONE', #27419, #6784, #13245, .T. ) ;
#486=EDGE_LOOP ( 'NONE', ( #7178, #9341, #8028, #31274 ) ) ;
#491=ORIENTED_EDGE ( 'NONE', *, *, #20535, .F. ) ;
#520=DIRECTION ( 'NONE',  ( -5.339440136655842133E-16, -1.000000000000000000, 6.938893903907197563E-17 ) ) ;
#561=DIRECTION ( 'NONE',  ( -5.339440136655842133E-16, -1.000000000000000000, 6.938893903907197563E-17 ) ) ;
#597=EDGE_CURVE ( 'NONE', #5418, #24725, #6477, .T. ) ;
#662=EDGE_LOOP ( 'NONE', ( #8266, #3117 ) ) ;
#686=ORIENTED_EDGE ( 'NONE', *, *, #188, .F. ) ;
#764=CIRCLE ( 'NONE', #26644, 4.725000000000016520 ) ;
#818=DIRECTION ( 'NONE',  ( -0.8432271980573220471, 4.875366479720417855E-16, 0.5375573387615479870 ) ) ;
#824=AXIS2_PLACEMENT_3D ( 'NONE', #33297, #24491, #5926 ) ;
#857=EDGE_CURVE ( 'NONE', #18809, #28617, #1930, .T. ) ;
#909=DIRECTION ( 'NONE',  ( 1.000000000000000000, -5.339440136655842133E-16, -1.047965281155519420E-16 ) ) ;
#911=ORIENTED_EDGE ( 'NONE', *, *, #959, .F. ) ;
#918=AXIS2_PLACEMENT_3D ( 'NONE', #32577, #332, #10621 ) ;
#959=EDGE_CURVE ( 'NONE', #8132, #34240, #13437, .T. ) ;
#979=AXIS2_PLACEMENT_3D ( 'NONE', #5322, #32316, #24399 ) ;
#997=AXIS2_PLACEMENT_3D ( 'NONE', #354, #27740, #13703 ) ;
#1000=DIRECTION ( 'NONE',  ( 1.000000000000000000, -5.339440136655842133E-16, -1.047965281155519420E-16 ) ) ;
#1007=DIRECTION ( 'NONE',  ( -1.000000000000000000, 5.339440136655842133E-16, 1.047965281155519420E-16 ) ) ;
#1042=FACE_OUTER_BOUND ( 'NONE', #18730, .T. ) ;
#1050=CARTESIAN_POINT ( 'NONE',  ( -2.000000000000001776, 6.765000000000020997, -2.775557561562891351E-14 ) ) ;
#1063=ORIENTED_EDGE ( 'NONE', *, *, #18291, .T. ) ;
#1099=CARTESIAN_POINT ( 'NONE',  ( 1.599999999999990985, -4.694161725993254197E-16, -6.765000000000044977 ) ) ;
#1128=CARTESIAN_POINT ( 'NONE',  ( 1.799999999999995604, 8.057851996059937582E-16, 4.200000000000014388 ) ) ;
#1179=CYLINDRICAL_SURFACE ( 'NONE', #28107, 8.000000000000051514 ) ;
#1219=AXIS2_PLACEMENT_3D ( 'NONE', #31997, #21184, #34528 ) ;
#1228=CIRCLE ( 'NONE', #27681, 0.1999999999999992339 ) ;
#1232=CARTESIAN_POINT ( 'NONE',  ( -1.999999999999998224, -1.846447412309851863E-16, -4.200000000000014388 ) ) ;
#1251=ORIENTED_EDGE ( 'NONE', *, *, #31643, .F. ) ;
#1345=DIRECTION ( 'NONE',  ( 1.000000000000000000, -5.339440136655842133E-16, -1.047965281155519420E-16 ) ) ;
#1465=CIRCLE ( 'NONE', #25055, 7.800000000000051337 ) ;
#1522=DIRECTION ( 'NONE',  ( 1.000000000000000000, -5.339440136655842133E-16, -1.047965281155519420E-16 ) ) ;
#1594=DIRECTION ( 'NONE',  ( 8.708451184622495809E-17, -6.938893903907203726E-17, -1.000000000000000000 ) ) ;
#1606=ORIENTED_EDGE ( 'NONE', *, *, #30212, .F. ) ;
#1647=ORIENTED_EDGE ( 'NONE', *, *, #13808, .T. ) ;
#1664=DIRECTION ( 'NONE',  ( 1.000000000000000000, -5.339440136655842133E-16, -1.047965281155519420E-16 ) ) ;
#1667=DIRECTION ( 'NONE',  ( 1.000000000000000000, -5.339440136655842133E-16, -1.047965281155519420E-16 ) ) ;
#1677=CARTESIAN_POINT ( 'NONE',  ( -1.520000000000000018, -3.261632136597012339E-16, -5.016000000000010672 ) ) ;
#1696=EDGE_LOOP ( 'NONE', ( #7796, #14510 ) ) ;
#1704=CARTESIAN_POINT ( 'NONE',  ( -2.000000000000001776, 0.000000000000000000, 0.000000000000000000 ) ) ;
#1715=CARTESIAN_POINT ( 'NONE',  ( -1.799999999999996048, 0.000000000000000000, 0.000000000000000000 ) ) ;
#1718=DIRECTION ( 'NONE',  ( -1.047965281155519913E-16, -6.938893903907192632E-17, -1.000000000000000000 ) ) ;
#1727=ORIENTED_EDGE ( 'NONE', *, *, #3412, .F. ) ;
#1780=EDGE_LOOP ( 'NONE', ( #22222, #6075 ) ) ;
#1841=EDGE_CURVE ( 'NONE', #2812, #27419, #31874, .T. ) ;
#1875=CARTESIAN_POINT ( 'NONE',  ( -90.00000000000002842, 0.000000000000000000, 6.938893903907228378E-15 ) ) ;
#1877=CARTESIAN_POINT ( 'NONE',  ( -90.00000000000002842, -3.455569164145799535E-16, -4.980000000000010196 ) ) ;
#1879=TOROIDAL_SURFACE ( 'NONE', #9930, 6.983999999999990216, 0.04100000000000673939 ) ;
#1890=EDGE_LOOP ( 'NONE', ( #6488, #9616, #27724, #30292 ) ) ;
#1901=AXIS2_PLACEMENT_3D ( 'NONE', #34945, #12784, #12963 ) ;
#1906=DIRECTION ( 'NONE',  ( 1.000000000000000000, -5.339440136655842133E-16, -1.047965281155519420E-16 ) ) ;
#1930=CIRCLE ( 'NONE', #27805, 6.765000000000044977 ) ;
#1977=FACE_BOUND ( 'NONE', #1696, .T. ) ;
#1980=DIRECTION ( 'NONE',  ( 0.8432271980573220471, -4.875366479720417855E-16, -0.5375573387615479870 ) ) ;
#2025=DIRECTION ( 'NONE',  ( 8.708451184622495809E-17, -6.938893903907203726E-17, -1.000000000000000000 ) ) ;
#2030=AXIS2_PLACEMENT_3D ( 'NONE', #10176, #9640, #31425 ) ;
#2058=DIRECTION ( 'NONE',  ( 1.000000000000000000, -5.339440136655842133E-16, -1.047965281155519420E-16 ) ) ;
#2060=DIRECTION ( 'NONE',  ( 5.339440136655842133E-16, 1.000000000000000000, -1.918536189538073087E-16 ) ) ;
#2130=DIRECTION ( 'NONE',  ( 1.000000000000000000, -5.339440136655839175E-16, 0.000000000000000000 ) ) ;
#2145=DIRECTION ( 'NONE',  ( 1.000000000000000000, -5.339440136655842133E-16, -1.047965281155519420E-16 ) ) ;
#2152=DIRECTION ( 'NONE',  ( 1.047965281155515106E-16, -6.938893903907203726E-17, -1.000000000000000000 ) ) ;
#2154=EDGE_LOOP ( 'NONE', ( #32633, #8100, #15394, #33809 ) ) ;
#2184=LINE ( 'NONE', #23948, #2502 ) ;
#2231=CIRCLE ( 'NONE', #18875, 8.000000000000051514 ) ;
#2247=DIRECTION ( 'NONE',  ( 9.615983791445651082E-17, -6.938893903907203726E-17, -1.000000000000000000 ) ) ;
#2277=DIRECTION ( 'NONE',  ( -1.000000000000000000, 5.339440136655861854E-16, 0.000000000000000000 ) ) ;
#2293=ORIENTED_EDGE ( 'NONE', *, *, #2616, .T. ) ;
#2310=CARTESIAN_POINT ( 'NONE',  ( -1.479000000000007420, -4.846123502488801633E-16, -6.984000000000015085 ) ) ;
#2347=DIRECTION ( 'NONE',  ( 1.084202172485500613E-16, -6.938893903907203726E-17, -1.000000000000000000 ) ) ;
#2415=DIRECTION ( 'NONE',  ( -1.047965281155519913E-16, -6.938893903907192632E-17, -1.000000000000000000 ) ) ;
#2426=AXIS2_PLACEMENT_3D ( 'NONE', #4905, #31716, #7048 ) ;
#2431=CYLINDRICAL_SURFACE ( 'NONE', #25329, 4.980000000000017302 ) ;
#2440=CARTESIAN_POINT ( 'NONE',  ( 2.000000000000002665, 1.462249188368523427E-15, 7.800000000000023803 ) ) ;
#2442=LINE ( 'NONE', #10894, #13963 ) ;
#2443=DIRECTION ( 'NONE',  ( 5.339440136655842133E-16, 1.000000000000000000, -1.918536189538073087E-16 ) ) ;
#2449=CARTESIAN_POINT ( 'NONE',  ( 1.498621416870293155, -4.936931676003361682E-14, -7.020000000000020890 ) ) ;
#2491=EDGE_LOOP ( 'NONE', ( #14434, #3402, #29476, #33688 ) ) ;
#2502=VECTOR ( 'NONE', #35296, 1000.000000000000000 ) ;
#2546=ORIENTED_EDGE ( 'NONE', *, *, #31900, .T. ) ;
#2573=DIRECTION ( 'NONE',  ( 1.047965281155515106E-16, -6.938893903907203726E-17, -1.000000000000000000 ) ) ;
#2580=DIRECTION ( 'NONE',  ( 1.000000000000000000, -5.339440136655834244E-16, 0.000000000000000000 ) ) ;
#2591=CARTESIAN_POINT ( 'NONE',  ( 2.000000000000002665, -4.771817072227797033E-14, 6.765000000000020997 ) ) ;
#2596=CARTESIAN_POINT ( 'NONE',  ( 1.599999999999990985, -4.871103520542888323E-16, -7.020000000000045759 ) ) ;
#2597=ORIENTED_EDGE ( 'NONE', *, *, #11936, .T. ) ;
#2600=DIRECTION ( 'NONE',  ( 1.000000000000000000, -5.339440136655842133E-16, -1.047965281155519420E-16 ) ) ;
#2616=EDGE_CURVE ( 'NONE', #34867, #19376, #7075, .T. ) ;
#2645=CARTESIAN_POINT ( 'NONE',  ( 2.000000000000002220, 4.434986294202125852E-16, 4.724999999999999645 ) ) ;
#2704=CIRCLE ( 'NONE', #18196, 0.04099999999999937028 ) ;
#2751=ORIENTED_EDGE ( 'NONE', *, *, #26717, .T. ) ;
#2756=CARTESIAN_POINT ( 'NONE',  ( -2.000000000000000888, 1.569037991101640822E-15, 7.800000000000023803 ) ) ;
#2787=VERTEX_POINT ( 'NONE', #33745 ) ;
#2812=VERTEX_POINT ( 'NONE', #12134 ) ;
#2839=CARTESIAN_POINT ( 'NONE',  ( 1.520000000000018447, -3.699466227802803499E-16, -5.016000000000010672 ) ) ;
#2944=EDGE_CURVE ( 'NONE', #6784, #32680, #30679, .T. ) ;
#2965=TOROIDAL_SURFACE ( 'NONE', #4122, 7.800000000000023803, 0.2000000000000003164 ) ;
#2993=ORIENTED_EDGE ( 'NONE', *, *, #857, .T. ) ;
#3007=DIRECTION ( 'NONE',  ( -1.000000000000000000, 5.339440136655842133E-16, -1.047965281155515476E-16 ) ) ;
#3039=CARTESIAN_POINT ( 'NONE',  ( 2.000000000000001776, 7.800000000000029132, 3.469446951953614189E-15 ) ) ;
#3061=DIRECTION ( 'NONE',  ( 8.708451184622495809E-17, -6.938893903907203726E-17, -1.000000000000000000 ) ) ;
#3077=COLOUR_RGB ( '', 0.31764706, 0.68627451, 0.89019608) ;
#3090=ADVANCED_FACE ( 'NONE', ( #3845 ), #1879, .T. ) ;
#3092=ADVANCED_FACE ( 'NONE', ( #31373 ), #30043, .T. ) ;
#3112=AXIS2_PLACEMENT_3D ( 'NONE', #28363, #1007, #33578 ) ;
#3117=ORIENTED_EDGE ( 'NONE', *, *, #23985, .F. ) ;
#3123=SHAPE_REPRESENTATION_RELATIONSHIP ( 'NONE' , 'NONE' ,  #31430, #19774 ) ;
#3292=AXIS2_PLACEMENT_3D ( 'NONE', #1875, #35005, #18769 ) ;
#3302=( LENGTH_UNIT ( ) NAMED_UNIT ( * ) SI_UNIT ( .MILLI., .METRE. ) );
#3317=AXIS2_PLACEMENT_3D ( 'NONE', #10394, #21351, #21710 ) ;
#3337=CIRCLE ( 'NONE', #13108, 6.984000000000015085 ) ;
#3344=VERTEX_POINT ( 'NONE', #2756 ) ;
#3349=AXIS2_PLACEMENT_3D ( 'NONE', #22314, #5422, #8627 ) ;
#3402=ORIENTED_EDGE ( 'NONE', *, *, #431, .T. ) ;
#3412=EDGE_CURVE ( 'NONE', #8708, #21509, #24870, .T. ) ;
#3441=AXIS2_PLACEMENT_3D ( 'NONE', #32344, #21349, #13444 ) ;
#3477=SURFACE_STYLE_USAGE ( .BOTH. , #17127 ) ;
#3552=EDGE_LOOP ( 'NONE', ( #35355, #12838, #3978, #32315 ) ) ;
#3573=DIRECTION ( 'NONE',  ( 1.000000000000000000, -5.339440136655842133E-16, -1.047965281155519420E-16 ) ) ;
#3599=ORIENTED_EDGE ( 'NONE', *, *, #31643, .T. ) ;
#3602=ORIENTED_EDGE ( 'NONE', *, *, #29308, .T. ) ;
#3733=EDGE_CURVE ( 'NONE', #10764, #30393, #2184, .T. ) ;
#3745=ADVANCED_FACE ( 'NONE', ( #4529 ), #21571, .F. ) ;
#3791=ORIENTED_EDGE ( 'NONE', *, *, #23520, .F. ) ;
#3845=FACE_OUTER_BOUND ( 'NONE', #12614, .T. ) ;
#3927=SHAPE_DEFINITION_REPRESENTATION ( #30770, #31430 ) ;
#3963=DIRECTION ( 'NONE',  ( 8.708451184622495809E-17, -6.938893903907203726E-17, -1.000000000000000000 ) ) ;
#3978=ORIENTED_EDGE ( 'NONE', *, *, #17424, .T. ) ;
#3990=AXIS2_PLACEMENT_3D ( 'NONE', #35024, #21301, #7619 ) ;
#4019=CIRCLE ( 'NONE', #19505, 0.1999999999999998723 ) ;
#4056=ORIENTED_EDGE ( 'NONE', *, *, #34152, .F. ) ;
#4072=CARTESIAN_POINT ( 'NONE',  ( 1.498621416870293821, 0.000000000000000000, 0.000000000000000000 ) ) ;
#4083=CARTESIAN_POINT ( 'NONE',  ( -1.799999999999996048, 0.000000000000000000, 0.000000000000000000 ) ) ;
#4122=AXIS2_PLACEMENT_3D ( 'NONE', #33510, #19985, #28297 ) ;
#4155=STYLED_ITEM ( 'NONE', ( #23497 ), #22590 ) ;
#4191=CARTESIAN_POINT ( 'NONE',  ( -1.799999999999996048, 1.534828951630468330E-15, 8.000000000000051514 ) ) ;
#4245=CARTESIAN_POINT ( 'NONE',  ( -1.519999999999993578, 0.000000000000000000, 0.000000000000000000 ) ) ;
#4390=EDGE_CURVE ( 'NONE', #6784, #32201, #24383, .T. ) ;
#4399=AXIS2_PLACEMENT_3D ( 'NONE', #6904, #20573, #29240 ) ;
#4401=CIRCLE ( 'NONE', #28517, 7.020000000000045759 ) ;
#4404=DIRECTION ( 'NONE',  ( -1.000000000000000000, 5.339440136655836216E-16, 0.000000000000000000 ) ) ;
#4430=( LENGTH_UNIT ( ) NAMED_UNIT ( * ) SI_UNIT ( .MILLI., .METRE. ) );
#4529=FACE_OUTER_BOUND ( 'NONE', #30724, .T. ) ;
#4534=VERTEX_POINT ( 'NONE', #7632 ) ;
#4700=DIRECTION ( 'NONE',  ( 1.000000000000000000, -5.339440136655842133E-16, -1.047965281155519420E-16 ) ) ;
#4762=DIRECTION ( 'NONE',  ( 1.000000000000000000, -5.339440136655842133E-16, -1.047965281155519420E-16 ) ) ;
#4782=AXIS2_PLACEMENT_3D ( 'NONE', #10707, #19324, #30338 ) ;
#4792=DIRECTION ( 'NONE',  ( 9.178431089824344374E-17, -6.938893903907203726E-17, -1.000000000000000000 ) ) ;
#4797=CARTESIAN_POINT ( 'NONE',  ( -1.599999999999989875, -4.627228502943551802E-14, 4.980000000000000426 ) ) ;
#4815=DIRECTION ( 'NONE',  ( 9.178431089824344374E-17, -6.938893903907203726E-17, -1.000000000000000000 ) ) ;
#4820=ORIENTED_EDGE ( 'NONE', *, *, #27797, .F. ) ;
#4823=LINE ( 'NONE', #7145, #15357 ) ;
#4905=CARTESIAN_POINT ( 'NONE',  ( 1.799999999999996048, 0.000000000000000000, 0.000000000000000000 ) ) ;
#4944=ORIENTED_EDGE ( 'NONE', *, *, #26740, .F. ) ;
#4962=AXIS2_PLACEMENT_3D ( 'NONE', #17066, #520, #25375 ) ;
#4963=FACE_BOUND ( 'NONE', #20149, .T. ) ;
#4972=ORIENTED_EDGE ( 'NONE', *, *, #4390, .F. ) ;
#5018=ORIENTED_EDGE ( 'NONE', *, *, #22614, .F. ) ;
#5024=CIRCLE ( 'NONE', #6720, 6.765000000000044977 ) ;
#5064=CIRCLE ( 'NONE', #15951, 7.020000000000045759 ) ;
#5065=VERTEX_POINT ( 'NONE', #21578 ) ;
#5083=EDGE_LOOP ( 'NONE', ( #7070, #31003, #30832, #16173 ) ) ;
#5148=EDGE_CURVE ( 'NONE', #29518, #34240, #7727, .T. ) ;
#5195=CIRCLE ( 'NONE', #12662, 7.020000000000045759 ) ;
#5210=AXIS2_PLACEMENT_3D ( 'NONE', #7374, #10787, #2347 ) ;
#5241=ORIENTED_EDGE ( 'NONE', *, *, #29308, .F. ) ;
#5267=DIRECTION ( 'NONE',  ( 0.000000000000000000, -6.938893903907203726E-17, -1.000000000000000000 ) ) ;
#5279=EDGE_CURVE ( 'NONE', #25119, #16586, #7174, .T. ) ;
#5300=CARTESIAN_POINT ( 'NONE',  ( 2.000000000000002665, -5.412337245047654898E-16, -7.800000000000051337 ) ) ;
#5303=AXIS2_PLACEMENT_3D ( 'NONE', #9310, #31099, #6423 ) ;
#5322=CARTESIAN_POINT ( 'NONE',  ( 1.799999999999996936, -5.412337245047654898E-16, -7.800000000000051337 ) ) ;
#5334=DIRECTION ( 'NONE',  ( 1.282131172192753642E-16, -6.938893903907203726E-17, -1.000000000000000000 ) ) ;
#5353=DIRECTION ( 'NONE',  ( -1.047965281155515106E-16, 6.938893903907203726E-17, 1.000000000000000000 ) ) ;
#5373=AXIS2_PLACEMENT_3D ( 'NONE', #15870, #18406, #27061 ) ;
#5418=VERTEX_POINT ( 'NONE', #20110 ) ;
#5422=DIRECTION ( 'NONE',  ( 1.000000000000000000, -5.339440136655842133E-16, -1.047965281155519420E-16 ) ) ;
#5438=FACE_OUTER_BOUND ( 'NONE', #5083, .T. ) ;
#5448=AXIS2_PLACEMENT_3D ( 'NONE', #16888, #27892, #10810 ) ;
#5476=LINE ( 'NONE', #29432, #29933 ) ;
#5544=VECTOR ( 'NONE', #22343, 1000.000000000000000 ) ;
#5546=ORIENTED_EDGE ( 'NONE', *, *, #17697, .F. ) ;
#5599=ORIENTED_EDGE ( 'NONE', *, *, #5279, .T. ) ;
#5639=ORIENTED_EDGE ( 'NONE', *, *, #25143, .T. ) ;
#5716=UNCERTAINTY_MEASURE_WITH_UNIT (LENGTH_MEASURE( 1.000000000000000082E-05 ), #3302, 'distance_accuracy_value', 'NONE');
#5752=CARTESIAN_POINT ( 'NONE',  ( -1.599999999999990319, 0.000000000000000000, 0.000000000000000000 ) ) ;
#5796=AXIS2_PLACEMENT_3D ( 'NONE', #33814, #3573, #22457 ) ;
#5825=DIRECTION ( 'NONE',  ( 1.000000000000000000, -5.339440136655842133E-16, -1.047965281155519420E-16 ) ) ;
#5855=AXIS2_PLACEMENT_3D ( 'NONE', #30451, #16739, #14041 ) ;
#5863=TOROIDAL_SURFACE ( 'NONE', #27796, 7.800000000000023803, 0.1999999999999992339 ) ;
#5878=DIRECTION ( 'NONE',  ( 1.000000000000000000, -5.339440136655842133E-16, -1.047965281155519420E-16 ) ) ;
#5900=ORIENTED_EDGE ( 'NONE', *, *, #34888, .F. ) ;
#5926=DIRECTION ( 'NONE',  ( 1.112002228190253556E-16, -6.938893903907203726E-17, -1.000000000000000000 ) ) ;
#5940=ORIENTED_EDGE ( 'NONE', *, *, #28004, .F. ) ;
#5967=CARTESIAN_POINT ( 'NONE',  ( -90.00000000000002842, 1.534828951630468922E-15, 8.000000000000058620 ) ) ;
#6026=CARTESIAN_POINT ( 'NONE',  ( 2.000000000000001776, 0.000000000000000000, 0.000000000000000000 ) ) ;
#6036=CARTESIAN_POINT ( 'NONE',  ( -1.799999999999996048, 0.000000000000000000, 0.000000000000000000 ) ) ;
#6054=CIRCLE ( 'NONE', #12374, 0.2000000000000003164 ) ;
#6064=ORIENTED_EDGE ( 'NONE', *, *, #19613, .F. ) ;
#6075=ORIENTED_EDGE ( 'NONE', *, *, #22614, .T. ) ;
#6146=CARTESIAN_POINT ( 'NONE',  ( 1.799999999999996936, -5.551115123125799465E-16, -8.000000000000051514 ) ) ;
#6227=FACE_OUTER_BOUND ( 'NONE', #34921, .T. ) ;
#6316=DIRECTION ( 'NONE',  ( -8.708451184622495809E-17, 6.938893903907203726E-17, 1.000000000000000000 ) ) ;
#6403=FACE_OUTER_BOUND ( 'NONE', #3552, .T. ) ;
#6423=DIRECTION ( 'NONE',  ( 9.266685234918781277E-17, -6.938893903907202493E-17, -1.000000000000000000 ) ) ;
#6477=CIRCLE ( 'NONE', #28929, 6.765000000000044977 ) ;
#6488=ORIENTED_EDGE ( 'NONE', *, *, #11988, .T. ) ;
#6494=DIRECTION ( 'NONE',  ( 1.000000000000000000, -5.339440136655853966E-16, 0.000000000000000000 ) ) ;
#6540=CIRCLE ( 'NONE', #26671, 4.000000000000014211 ) ;
#6552=VECTOR ( 'NONE', #18363, 1000.000000000000000 ) ;
#6605=CARTESIAN_POINT ( 'NONE',  ( -1.799999999999995604, -2.914335439641035426E-16, -4.200000000000014388 ) ) ;
#6608=FACE_OUTER_BOUND ( 'NONE', #29501, .T. ) ;
#6618=DIRECTION ( 'NONE',  ( -1.047965281155519913E-16, -6.938893903907192632E-17, -1.000000000000000000 ) ) ;
#6632=CARTESIAN_POINT ( 'NONE',  ( -1.599999999999990319, 0.000000000000000000, 0.000000000000000000 ) ) ;
#6651=ORIENTED_EDGE ( 'NONE', *, *, #28678, .F. ) ;
#6654=FACE_OUTER_BOUND ( 'NONE', #162, .T. ) ;
#6687=AXIS2_PLACEMENT_3D ( 'NONE', #21446, #13723, #2573 ) ;
#6709=AXIS2_PLACEMENT_3D ( 'NONE', #13898, #24886, #8661 ) ;
#6720=AXIS2_PLACEMENT_3D ( 'NONE', #19550, #33793, #11466 ) ;
#6757=DIRECTION ( 'NONE',  ( 0.000000000000000000, -6.938893903907202493E-17, -1.000000000000000000 ) ) ;
#6767=CARTESIAN_POINT ( 'NONE',  ( 1.599999999999990319, 0.000000000000000000, 0.000000000000000000 ) ) ;
#6781=EDGE_CURVE ( 'NONE', #2812, #32201, #27240, .T. ) ;
#6784=VERTEX_POINT ( 'NONE', #21815 ) ;
#6792=FACE_OUTER_BOUND ( 'NONE', #32560, .T. ) ;
#6826=LINE ( 'NONE', #9350, #31114 ) ;
#6835=DIRECTION ( 'NONE',  ( -1.000000000000000000, 5.339440136655842133E-16, -1.047965281155515476E-16 ) ) ;
#6854=ADVANCED_FACE ( 'NONE', ( #11382 ), #30636, .T. ) ;
#6904=CARTESIAN_POINT ( 'NONE',  ( -1.799999999999996936, 1.496458227839707357E-15, 7.800000000000051337 ) ) ;
#6934=DIRECTION ( 'NONE',  ( 1.000000000000000000, -5.339440136655842133E-16, -1.047965281155519420E-16 ) ) ;
#6953=AXIS2_PLACEMENT_3D ( 'NONE', #12486, #31571, #29238 ) ;
#6977=DIRECTION ( 'NONE',  ( -1.000000000000000000, 5.339440136655842133E-16, 1.047965281155519420E-16 ) ) ;
#7006=TOROIDAL_SURFACE ( 'NONE', #13355, 7.800000000000023803, 0.1999999999999992339 ) ;
#7041=EDGE_CURVE ( 'NONE', #10764, #11716, #24537, .T. ) ;
#7048=DIRECTION ( 'NONE',  ( 1.084202172485497408E-16, -6.938893903907204958E-17, -1.000000000000000000 ) ) ;
#7064=VERTEX_POINT ( 'NONE', #6146 ) ;
#7070=ORIENTED_EDGE ( 'NONE', *, *, #435, .F. ) ;
#7075=CIRCLE ( 'NONE', #31236, 6.765000000000044977 ) ;
#7083=ORIENTED_EDGE ( 'NONE', *, *, #2944, .T. ) ;
#7091=EDGE_CURVE ( 'NONE', #32201, #21788, #2704, .T. ) ;
#7120=DIRECTION ( 'NONE',  ( -9.178431089824344374E-17, 6.938893903907203726E-17, 1.000000000000000000 ) ) ;
#7122=ORIENTED_EDGE ( 'NONE', *, *, #34922, .T. ) ;
#7145=CARTESIAN_POINT ( 'NONE',  ( -1.599999999999990763, 9.554310223899640008E-16, 4.980000000000017302 ) ) ;
#7174=CIRCLE ( 'NONE', #19246, 6.765000000000044977 ) ;
#7178=ORIENTED_EDGE ( 'NONE', *, *, #7952, .T. ) ;
#7335=CARTESIAN_POINT ( 'NONE',  ( 1.799999999999996048, 0.000000000000000000, 0.000000000000000000 ) ) ;
#7340=TOROIDAL_SURFACE ( 'NONE', #3349, 6.983999999999990216, 0.04100000000000673939 ) ;
#7356=ORIENTED_EDGE ( 'NONE', *, *, #27956, .F. ) ;
#7374=CARTESIAN_POINT ( 'NONE',  ( -1.799999999999996048, 0.000000000000000000, 0.000000000000000000 ) ) ;
#7415=ORIENTED_EDGE ( 'NONE', *, *, #9816, .T. ) ;
#7580=ORIENTED_EDGE ( 'NONE', *, *, #10023, .T. ) ;
#7619=DIRECTION ( 'NONE',  ( 0.000000000000000000, -6.938893903907203726E-17, -1.000000000000000000 ) ) ;
#7632=CARTESIAN_POINT ( 'NONE',  ( -1.999999999999999112, 9.125740023391120405E-16, 4.200000000000014388 ) ) ;
#7685=ORIENTED_EDGE ( 'NONE', *, *, #2616, .F. ) ;
#7727=LINE ( 'NONE', #18710, #6552 ) ;
#7732=CARTESIAN_POINT ( 'NONE',  ( -2.000000000000001776, 0.000000000000000000, 0.000000000000000000 ) ) ;
#7757=EDGE_LOOP ( 'NONE', ( #34126, #16573 ) ) ;
#7774=EDGE_CURVE ( 'NONE', #34245, #27419, #4823, .T. ) ;
#7785=FACE_OUTER_BOUND ( 'NONE', #31155, .T. ) ;
#7796=ORIENTED_EDGE ( 'NONE', *, *, #34152, .T. ) ;
#7801=CARTESIAN_POINT ( 'NONE',  ( -1.519999999999992912, 1.359543261233475143E-15, 6.983999999999990216 ) ) ;
#7805=FACE_OUTER_BOUND ( 'NONE', #22139, .T. ) ;
#7839=ORIENTED_EDGE ( 'NONE', *, *, #20702, .F. ) ;
#7852=PLANE ( 'NONE',  #33220 ) ;
#7869=DIRECTION ( 'NONE',  ( -5.339440136655842133E-16, -1.000000000000000000, 6.938893903907197563E-17 ) ) ;
#7880=EDGE_CURVE ( 'NONE', #15577, #21509, #32064, .T. ) ;
#7881=EDGE_LOOP ( 'NONE', ( #20022, #19040 ) ) ;
#7900=CARTESIAN_POINT ( 'NONE',  ( -90.00000000000002842, 0.000000000000000000, 6.938893903907228378E-15 ) ) ;
#7931=DIRECTION ( 'NONE',  ( -9.266685234918781277E-17, 8.062994716340199375E-15, 1.000000000000000000 ) ) ;
#7952=EDGE_CURVE ( 'NONE', #14603, #30739, #17682, .T. ) ;
#7985=ADVANCED_FACE ( 'NONE', ( #16480, #24256 ), #7852, .T. ) ;
#8028=ORIENTED_EDGE ( 'NONE', *, *, #11988, .F. ) ;
#8037=CARTESIAN_POINT ( 'NONE',  ( -1.799999999999996048, 0.000000000000000000, 0.000000000000000000 ) ) ;
#8045=CYLINDRICAL_SURFACE ( 'NONE', #22235, 6.765000000000044977 ) ;
#8051=DIRECTION ( 'NONE',  ( 1.000000000000000000, -5.339440136655842133E-16, 1.047965281155515476E-16 ) ) ;
#8100=ORIENTED_EDGE ( 'NONE', *, *, #3412, .T. ) ;
#8105=AXIS2_PLACEMENT_3D ( 'NONE', #183, #8466, #27741 ) ;
#8127=COLOUR_RGB ( '', 0.31764706, 0.68627451, 0.89019608) ;
#8130=AXIS2_PLACEMENT_3D ( 'NONE', #18110, #26595, #4815 ) ;
#8132=VERTEX_POINT ( 'NONE', #8482 ) ;
#8161=ADVANCED_FACE ( 'NONE', ( #5438 ), #14802, .T. ) ;
#8168=ORIENTED_EDGE ( 'NONE', *, *, #25979, .F. ) ;
#8210=CARTESIAN_POINT ( 'NONE',  ( -2.000000000000001776, 4.724999999999993427, 0.000000000000000000 ) ) ;
#8266=ORIENTED_EDGE ( 'NONE', *, *, #16639, .F. ) ;
#8337=LINE ( 'NONE', #27804, #31249 ) ;
#8345=EDGE_LOOP ( 'NONE', ( #23372, #22145, #34646, #17959 ) ) ;
#8381=CIRCLE ( 'NONE', #824, 7.800000000000051337 ) ;
#8460=FACE_OUTER_BOUND ( 'NONE', #20580, .T. ) ;
#8466=DIRECTION ( 'NONE',  ( 1.000000000000000000, -5.339440136655842133E-16, -1.047965281155519420E-16 ) ) ;
#8482=CARTESIAN_POINT ( 'NONE',  ( 1.599999999999990763, -3.455569164145799535E-16, -4.980000000000017302 ) ) ;
#8487=AXIS2_PLACEMENT_3D ( 'NONE', #19782, #30795, #24047 ) ;
#8508=ORIENTED_EDGE ( 'NONE', *, *, #2944, .F. ) ;
#8512=ORIENTED_EDGE ( 'NONE', *, *, #188, .T. ) ;
#8620=ORIENTED_EDGE ( 'NONE', *, *, #13808, .F. ) ;
#8627=DIRECTION ( 'NONE',  ( -1.047965281155519790E-16, -6.938893903907192632E-17, -1.000000000000000000 ) ) ;
#8658=CARTESIAN_POINT ( 'NONE',  ( 1.498621416870377088, 0.000000000000000000, 0.000000000000000000 ) ) ;
#8660=ORIENTED_EDGE ( 'NONE', *, *, #7952, .F. ) ;
#8661=DIRECTION ( 'NONE',  ( 0.000000000000000000, -6.938893903907204958E-17, -1.000000000000000000 ) ) ;
#8708=VERTEX_POINT ( 'NONE', #25903 ) ;
#8715=ORIENTED_EDGE ( 'NONE', *, *, #4390, .T. ) ;
#8762=VERTEX_POINT ( 'NONE', #1232 ) ;
#8798=AXIS2_PLACEMENT_3D ( 'NONE', #32389, #27348, #24646 ) ;
#8830=CARTESIAN_POINT ( 'NONE',  ( -90.00000000000002842, -4.694161725993254197E-16, -6.765000000000038760 ) ) ;
#8851=FILL_AREA_STYLE ('',( #25435 ) ) ;
#8877=ORIENTED_EDGE ( 'NONE', *, *, #15601, .T. ) ;
#8895=ORIENTED_EDGE ( 'NONE', *, *, #10063, .T. ) ;
#8906=CARTESIAN_POINT ( 'NONE',  ( -90.00000000000002842, 0.000000000000000000, 6.938893903907228378E-15 ) ) ;
#8954=PLANE ( 'NONE',  #30663 ) ;
#9037=( NAMED_UNIT ( * ) PLANE_ANGLE_UNIT ( ) SI_UNIT ( $, .RADIAN. ) );
#9100=EDGE_LOOP ( 'NONE', ( #10994, #22771 ) ) ;
#9116=ORIENTED_EDGE ( 'NONE', *, *, #22505, .T. ) ;
#9126=DIRECTION ( 'NONE',  ( 0.000000000000000000, -6.938893903907203726E-17, -1.000000000000000000 ) ) ;
#9184=CIRCLE ( 'NONE', #5210, 4.000000000000014211 ) ;
#9228=CIRCLE ( 'NONE', #29374, 4.725000000000016520 ) ;
#9272=DIRECTION ( 'NONE',  ( 1.000000000000000000, -5.339440136655842133E-16, -1.047965281155519420E-16 ) ) ;
#9310=CARTESIAN_POINT ( 'NONE',  ( -1.498621416870293821, 0.000000000000000000, 0.000000000000000000 ) ) ;
#9314=FACE_BOUND ( 'NONE', #11516, .T. ) ;
#9320=DIRECTION ( 'NONE',  ( -1.047965281155515106E-16, 6.938893903907203726E-17, 1.000000000000000000 ) ) ;
#9341=ORIENTED_EDGE ( 'NONE', *, *, #9982, .T. ) ;
#9350=CARTESIAN_POINT ( 'NONE',  ( -90.00000000000002842, -2.775557561562891351E-16, -4.000000000000007105 ) ) ;
#9394=VERTEX_POINT ( 'NONE', #2440 ) ;
#9398=ORIENTED_EDGE ( 'NONE', *, *, #14308, .T. ) ;
#9399=CARTESIAN_POINT ( 'NONE',  ( 1.520000000000021334, 0.000000000000000000, 0.000000000000000000 ) ) ;
#9492=DIRECTION ( 'NONE',  ( -1.047965281155519790E-16, -6.938893903907192632E-17, -1.000000000000000000 ) ) ;
#9496=EDGE_CURVE ( 'NONE', #23013, #15452, #5064, .T. ) ;
#9528=CONICAL_SURFACE ( 'NONE', #22189, 4.725000000000016520, 0.5675376247847534472 ) ;
#9529=ORIENTED_EDGE ( 'NONE', *, *, #23165, .F. ) ;
#9616=ORIENTED_EDGE ( 'NONE', *, *, #30212, .T. ) ;
#9640=DIRECTION ( 'NONE',  ( 5.339440136655842133E-16, 1.000000000000000000, -1.918536189538073087E-16 ) ) ;
#9672=AXIS2_PLACEMENT_3D ( 'NONE', #12605, #6835, #34750 ) ;
#9676=DIRECTION ( 'NONE',  ( 1.084202172485500613E-16, -6.938893903907203726E-17, -1.000000000000000000 ) ) ;
#9700=ORIENTED_EDGE ( 'NONE', *, *, #9816, .F. ) ;
#9746=VERTEX_POINT ( 'NONE', #29231 ) ;
#9816=EDGE_CURVE ( 'NONE', #16768, #33264, #3337, .T. ) ;
#9840=CYLINDRICAL_SURFACE ( 'NONE', #29863, 6.765000000000044977 ) ;
#9930=AXIS2_PLACEMENT_3D ( 'NONE', #18032, #20901, #14805 ) ;
#9946=EDGE_CURVE ( 'NONE', #23989, #30393, #12620, .T. ) ;
#9982=EDGE_CURVE ( 'NONE', #30739, #24774, #28114, .T. ) ;
#10019=DIRECTION ( 'NONE',  ( 1.000000000000000000, -5.339440136655842133E-16, -1.047965281155519420E-16 ) ) ;
#10023=EDGE_CURVE ( 'NONE', #24725, #19376, #11191, .T. ) ;
#10063=EDGE_CURVE ( 'NONE', #9746, #29518, #22952, .T. ) ;
#10091=ORIENTED_EDGE ( 'NONE', *, *, #463, .T. ) ;
#10174=CARTESIAN_POINT ( 'NONE',  ( -90.00000000000002842, 1.346812405055736621E-15, 7.020000000000052864 ) ) ;
#10176=CARTESIAN_POINT ( 'NONE',  ( 1.479000000000007642, 9.623377526722998283E-16, 5.016000000000010672 ) ) ;
#10213=DIRECTION ( 'NONE',  ( 1.000000000000000000, -5.339440136655842133E-16, -1.047965281155519420E-16 ) ) ;
#10335=AXIS2_PLACEMENT_3D ( 'NONE', #8658, #19625, #6316 ) ;
#10342=DIRECTION ( 'NONE',  ( -1.047965281155519790E-16, -6.938893903907192632E-17, -1.000000000000000000 ) ) ;
#10367=ADVANCED_FACE ( 'NONE', ( #13632 ), #30382, .T. ) ;
#10390=ORIENTED_EDGE ( 'NONE', *, *, #7880, .F. ) ;
#10394=CARTESIAN_POINT ( 'NONE',  ( -1.599999999999990319, 0.000000000000000000, 0.000000000000000000 ) ) ;
#10412=ADVANCED_FACE ( 'NONE', ( #6403 ), #25883, .T. ) ;
#10462=CIRCLE ( 'NONE', #97, 4.980000000000017302 ) ;
#10517=DIRECTION ( 'NONE',  ( 0.000000000000000000, -6.938893903907203726E-17, -1.000000000000000000 ) ) ;
#10544=AXIS2_PLACEMENT_3D ( 'NONE', #11503, #28021, #12160 ) ;
#10612=CYLINDRICAL_SURFACE ( 'NONE', #19458, 4.980000000000017302 ) ;
#10621=DIRECTION ( 'NONE',  ( 9.314451653655516225E-17, -6.938893903907203726E-17, -1.000000000000000000 ) ) ;
#10628=DIRECTION ( 'NONE',  ( 1.000000000000000000, -5.339440136655842133E-16, -1.047965281155519420E-16 ) ) ;
#10689=EDGE_LOOP ( 'NONE', ( #12752, #6064 ) ) ;
#10707=CARTESIAN_POINT ( 'NONE',  ( 1.479000000000007420, 1.339905674773393496E-15, 6.984000000000015085 ) ) ;
#10731=ORIENTED_EDGE ( 'NONE', *, *, #28365, .F. ) ;
#10736=CIRCLE ( 'NONE', #23953, 4.980000000000017302 ) ;
#10764=VERTEX_POINT ( 'NONE', #2449 ) ;
#10787=DIRECTION ( 'NONE',  ( 1.000000000000000000, -5.339440136655842133E-16, -1.047965281155519420E-16 ) ) ;
#10810=DIRECTION ( 'NONE',  ( 9.314451653655516225E-17, -6.938893903907203726E-17, -1.000000000000000000 ) ) ;
#10832=CARTESIAN_POINT ( 'NONE',  ( -1.799999999999996492, 8.057851996059937582E-16, 4.200000000000014388 ) ) ;
#10851=DIRECTION ( 'NONE',  ( 9.314451653655516225E-17, -6.938893903907203726E-17, -1.000000000000000000 ) ) ;
#10875=CIRCLE ( 'NONE', #22336, 7.800000000000051337 ) ;
#10894=CARTESIAN_POINT ( 'NONE',  ( -90.00000000000002842, 1.346812405055736621E-15, 7.020000000000052864 ) ) ;
#10895=FACE_OUTER_BOUND ( 'NONE', #9100, .T. ) ;
#10994=ORIENTED_EDGE ( 'NONE', *, *, #9496, .T. ) ;
#11009=EDGE_CURVE ( 'NONE', #5065, #8132, #28161, .T. ) ;
#11022=AXIS2_PLACEMENT_3D ( 'NONE', #14885, #31465, #9492 ) ;
#11087=EDGE_CURVE ( 'NONE', #8762, #4534, #14418, .T. ) ;
#11112=FACE_OUTER_BOUND ( 'NONE', #29860, .T. ) ;
#11136=DIRECTION ( 'NONE',  ( 9.178431089824344374E-17, -6.938893903907203726E-17, -1.000000000000000000 ) ) ;
#11138=ORIENTED_EDGE ( 'NONE', *, *, #463, .F. ) ;
#11191=LINE ( 'NONE', #8830, #18954 ) ;
#11237=VERTEX_POINT ( 'NONE', #19116 ) ;
#11382=FACE_OUTER_BOUND ( 'NONE', #486, .T. ) ;
#11424=DIRECTION ( 'NONE',  ( 1.000000000000000000, -5.339440136655842133E-16, -1.047965281155519420E-16 ) ) ;
#11427=AXIS2_PLACEMENT_3D ( 'NONE', #20178, #1664, #14796 ) ;
#11440=DIRECTION ( 'NONE',  ( -1.047965281155519667E-16, -6.938893903907193865E-17, -1.000000000000000000 ) ) ;
#11454=CARTESIAN_POINT ( 'NONE',  ( 1.498621416870377088, 0.000000000000000000, 0.000000000000000000 ) ) ;
#11466=DIRECTION ( 'NONE',  ( 9.615983791445651082E-17, -6.938893903907203726E-17, -1.000000000000000000 ) ) ;
#11478=ADVANCED_FACE ( 'NONE', ( #11904 ), #2965, .T. ) ;
#11489=AXIS2_PLACEMENT_3D ( 'NONE', #4245, #9272, #31943 ) ;
#11503=CARTESIAN_POINT ( 'NONE',  ( 1.599999999999990319, 0.000000000000000000, 0.000000000000000000 ) ) ;
#11516=EDGE_LOOP ( 'NONE', ( #29734, #7685 ) ) ;
#11523=EDGE_LOOP ( 'NONE', ( #33218, #2546, #2293, #21824 ) ) ;
#11524=AXIS2_PLACEMENT_3D ( 'NONE', #20283, #34179, #6618 ) ;
#11535=EDGE_CURVE ( 'NONE', #13171, #14603, #1228, .T. ) ;
#11564=( NAMED_UNIT ( * ) SI_UNIT ( $, .STERADIAN. ) SOLID_ANGLE_UNIT ( ) );
#11640=CARTESIAN_POINT ( 'NONE',  ( -90.00000000000002842, 0.000000000000000000, 6.938893903907228378E-15 ) ) ;
#11641=CIRCLE ( 'NONE', #19674, 6.765000000000044977 ) ;
#11716=VERTEX_POINT ( 'NONE', #25896 ) ;
#11762=CARTESIAN_POINT ( 'NONE',  ( 2.000000000000002220, 2.507828756375099332E-16, -4.725000000000016520 ) ) ;
#11814=ADVANCED_FACE ( 'NONE', ( #6608 ), #24260, .T. ) ;
#11816=DIRECTION ( 'NONE',  ( -1.000000000000000000, 5.339440136655843119E-16, 0.000000000000000000 ) ) ;
#11862=AXIS2_PLACEMENT_3D ( 'NONE', #29447, #26572, #6757 ) ;
#11904=FACE_OUTER_BOUND ( 'NONE', #1890, .T. ) ;
#11909=CIRCLE ( 'NONE', #24599, 7.020000000000045759 ) ;
#11924=DIRECTION ( 'NONE',  ( -1.000000000000000000, 5.339440136655840161E-16, 0.000000000000000000 ) ) ;
#11936=EDGE_CURVE ( 'NONE', #27419, #2812, #10462, .T. ) ;
#11988=EDGE_CURVE ( 'NONE', #7064, #24774, #15589, .T. ) ;
#12051=EDGE_LOOP ( 'NONE', ( #14533, #4056, #7580, #22935 ) ) ;
#12091=ORIENTED_EDGE ( 'NONE', *, *, #28004, .T. ) ;
#12105=ORIENTED_EDGE ( 'NONE', *, *, #20001, .F. ) ;
#12110=DIRECTION ( 'NONE',  ( 1.000000000000000000, -5.339440136655842133E-16, -1.047965281155519420E-16 ) ) ;
#12127=CARTESIAN_POINT ( 'NONE',  ( -1.519999999999993578, 0.000000000000000000, 0.000000000000000000 ) ) ;
#12134=CARTESIAN_POINT ( 'NONE',  ( -1.599999999999989875, -3.455569164145799535E-16, -4.980000000000017302 ) ) ;
#12148=CARTESIAN_POINT ( 'NONE',  ( -1.599999999999989653, -4.694161725993254197E-16, -6.765000000000044977 ) ) ;
#12160=DIRECTION ( 'NONE',  ( 8.708451184622495809E-17, -6.938893903907203726E-17, -1.000000000000000000 ) ) ;
#12166=DIRECTION ( 'NONE',  ( 8.708451184622495809E-17, -6.938893903907203726E-17, -1.000000000000000000 ) ) ;
#12174=EDGE_CURVE ( 'NONE', #11237, #18917, #26555, .T. ) ;
#12188=DIRECTION ( 'NONE',  ( 1.000000000000000000, -5.339440136655842133E-16, -1.047965281155519420E-16 ) ) ;
#12220=ORIENTED_EDGE ( 'NONE', *, *, #7091, .T. ) ;
#12224=AXIS2_PLACEMENT_3D ( 'NONE', #23633, #12110, #26339 ) ;
#12236=CIRCLE ( 'NONE', #32358, 0.2000000000000000944 ) ;
#12281=ORIENTED_EDGE ( 'NONE', *, *, #11087, .F. ) ;
#12336=CYLINDRICAL_SURFACE ( 'NONE', #11862, 7.020000000000045759 ) ;
#12348=DIRECTION ( 'NONE',  ( 9.266685234918781277E-17, -6.938893903907202493E-17, -1.000000000000000000 ) ) ;
#12364=CIRCLE ( 'NONE', #2030, 0.04100000000000673939 ) ;
#12374=AXIS2_PLACEMENT_3D ( 'NONE', #17564, #22976, #11816 ) ;
#12383=CARTESIAN_POINT ( 'NONE',  ( 2.000000000000001776, 0.000000000000000000, 0.000000000000000000 ) ) ;
#12393=EDGE_LOOP ( 'NONE', ( #32335, #8512, #12801, #5940 ) ) ;
#12428=ORIENTED_EDGE ( 'NONE', *, *, #9982, .F. ) ;
#12442=CARTESIAN_POINT ( 'NONE',  ( -1.799999999999995159, -5.412337245047654898E-16, -7.800000000000051337 ) ) ;
#12486=CARTESIAN_POINT ( 'NONE',  ( -2.000000000000001776, 0.000000000000000000, 0.000000000000000000 ) ) ;
#12520=SURFACE_STYLE_USAGE ( .BOTH. , #20411 ) ;
#12563=DIRECTION ( 'NONE',  ( 1.000000000000000000, -5.339440136655842133E-16, -1.047965281155519420E-16 ) ) ;
#12605=CARTESIAN_POINT ( 'NONE',  ( -1.519999999999993578, 6.984000000000004427, -4.163336342344337027E-14 ) ) ;
#12614=EDGE_LOOP ( 'NONE', ( #15302, #1647, #16182, #24021 ) ) ;
#12620=CIRCLE ( 'NONE', #23530, 7.020000000000045759 ) ;
#12662=AXIS2_PLACEMENT_3D ( 'NONE', #4072, #26190, #18072 ) ;
#12725=DIRECTION ( 'NONE',  ( 0.000000000000000000, 0.000000000000000000, 1.000000000000000000 ) ) ;
#12731=CARTESIAN_POINT ( 'NONE',  ( -90.00000000000002842, 1.297889732222515536E-15, 6.765000000000052083 ) ) ;
#12739=DIRECTION ( 'NONE',  ( 9.178431089824344374E-17, -6.938893903907203726E-17, -1.000000000000000000 ) ) ;
#12752=ORIENTED_EDGE ( 'NONE', *, *, #17168, .F. ) ;
#12784=DIRECTION ( 'NONE',  ( 1.000000000000000000, -5.339440136655842133E-16, -1.047965281155519420E-16 ) ) ;
#12801=ORIENTED_EDGE ( 'NONE', *, *, #10063, .F. ) ;
#12823=CARTESIAN_POINT ( 'NONE',  ( -1.599999999999990319, 0.000000000000000000, 0.000000000000000000 ) ) ;
#12838=ORIENTED_EDGE ( 'NONE', *, *, #20702, .T. ) ;
#12955=CARTESIAN_POINT ( 'NONE',  ( -1.599999999999989875, -3.455569164145799535E-16, -4.980000000000017302 ) ) ;
#12963=DIRECTION ( 'NONE',  ( 0.000000000000000000, -6.938893903907203726E-17, -1.000000000000000000 ) ) ;
#13011=ADVANCED_FACE ( 'NONE', ( #25545 ), #17834, .T. ) ;
#13052=AXIS2_PLACEMENT_3D ( 'NONE', #22878, #561, #6494 ) ;
#13060=VECTOR ( 'NONE', #818, 1000.000000000000114 ) ;
#13085=CARTESIAN_POINT ( 'NONE',  ( -1.519999999999992912, -4.846123502488801633E-16, -6.984000000000015085 ) ) ;
#13108=AXIS2_PLACEMENT_3D ( 'NONE', #26889, #24175, #10851 ) ;
#13152=DIRECTION ( 'NONE',  ( 0.000000000000000000, -6.938893903907203726E-17, -1.000000000000000000 ) ) ;
#13162=ORIENTED_EDGE ( 'NONE', *, *, #11535, .T. ) ;
#13171=VERTEX_POINT ( 'NONE', #21000 ) ;
#13245=LINE ( 'NONE', #27640, #32938 ) ;
#13315=DIRECTION ( 'NONE',  ( 1.000000000000000000, -5.339440136655842133E-16, -1.047965281155519420E-16 ) ) ;
#13355=AXIS2_PLACEMENT_3D ( 'NONE', #4083, #1906, #1718 ) ;
#13370=DIRECTION ( 'NONE',  ( 1.000000000000000000, -5.339440136655842133E-16, -1.047965281155519420E-16 ) ) ;
#13437=CIRCLE ( 'NONE', #5373, 4.980000000000017302 ) ;
#13444=DIRECTION ( 'NONE',  ( 8.645950338799857827E-17, -6.938893903907203726E-17, -1.000000000000000000 ) ) ;
#13446=AXIS2_PLACEMENT_3D ( 'NONE', #29309, #12563, #34709 ) ;
#13473=EDGE_LOOP ( 'NONE', ( #12428, #1063, #33228, #16154 ) ) ;
#13549=ORIENTED_EDGE ( 'NONE', *, *, #30883, .F. ) ;
#13632=FACE_OUTER_BOUND ( 'NONE', #34319, .T. ) ;
#13648=CIRCLE ( 'NONE', #18800, 0.04100000000000673939 ) ;
#13660=ORIENTED_EDGE ( 'NONE', *, *, #34825, .T. ) ;
#13663=FACE_OUTER_BOUND ( 'NONE', #27743, .T. ) ;
#13703=DIRECTION ( 'NONE',  ( 1.032573497605238773E-16, -6.938893903907203726E-17, -1.000000000000000000 ) ) ;
#13723=DIRECTION ( 'NONE',  ( 1.000000000000000000, -5.339440136655842133E-16, 1.047965281155515476E-16 ) ) ;
#13761=CARTESIAN_POINT ( 'NONE',  ( 1.799999999999996492, -4.728754675408722838E-14, 4.000000000000000000 ) ) ;
#13796=AXIS2_PLACEMENT_3D ( 'NONE', #27679, #5878, #16494 ) ;
#13808=EDGE_CURVE ( 'NONE', #16768, #11237, #13648, .T. ) ;
#13851=ADVANCED_FACE ( 'NONE', ( #10895, #4963 ), #21861, .T. ) ;
#13898=CARTESIAN_POINT ( 'NONE',  ( -90.00000000000002842, 0.000000000000000000, 6.938893903907228378E-15 ) ) ;
#13920=AXIS2_PLACEMENT_3D ( 'NONE', #6036, #19353, #11440 ) ;
#13963=VECTOR ( 'NONE', #26934, 1000.000000000000000 ) ;
#13978=DIRECTION ( 'NONE',  ( 1.000000000000000000, -5.339440136655842133E-16, -1.047965281155519420E-16 ) ) ;
#13993=DIRECTION ( 'NONE',  ( -1.047965281155519667E-16, -6.938893903907193865E-17, -1.000000000000000000 ) ) ;
#14001=DIRECTION ( 'NONE',  ( 1.000000000000000000, -5.339440136655842133E-16, 1.047965281155515476E-16 ) ) ;
#14022=DIRECTION ( 'NONE',  ( 1.000000000000000000, -5.339440136655842133E-16, -1.047965281155519420E-16 ) ) ;
#14041=DIRECTION ( 'NONE',  ( 9.266685234918781277E-17, 8.187894806610533430E-16, -1.000000000000000000 ) ) ;
#14097=DIRECTION ( 'NONE',  ( 1.000000000000000000, -5.339440136655842133E-16, -1.047965281155519420E-16 ) ) ;
#14135=CIRCLE ( 'NONE', #29085, 5.016000000000010672 ) ;
#14145=CIRCLE ( 'NONE', #34288, 4.980000000000017302 ) ;
#14171=ADVANCED_FACE ( 'NONE', ( #18093 ), #17667, .T. ) ;
#14288=CARTESIAN_POINT ( 'NONE',  ( -1.799999999999996048, -5.551115123125792563E-16, -8.000000000000051514 ) ) ;
#14308=EDGE_CURVE ( 'NONE', #30393, #23989, #4401, .T. ) ;
#14393=CIRCLE ( 'NONE', #14420, 0.2000000000000000944 ) ;
#14399=CARTESIAN_POINT ( 'NONE',  ( -90.00000000000002842, 7.674144758152321929E-16, 4.000000000000021316 ) ) ;
#14418=CIRCLE ( 'NONE', #6953, 4.200000000000014388 ) ;
#14420=AXIS2_PLACEMENT_3D ( 'NONE', #10832, #21602, #26864 ) ;
#14434=ORIENTED_EDGE ( 'NONE', *, *, #20003, .F. ) ;
#14478=DIRECTION ( 'NONE',  ( 1.084202172485497655E-16, -6.938893903907204958E-17, -1.000000000000000000 ) ) ;
#14497=VECTOR ( 'NONE', #21142, 1000.000000000000000 ) ;
#14510=ORIENTED_EDGE ( 'NONE', *, *, #597, .T. ) ;
#14533=ORIENTED_EDGE ( 'NONE', *, *, #31900, .F. ) ;
#14586=ORIENTED_EDGE ( 'NONE', *, *, #1841, .T. ) ;
#14603=VERTEX_POINT ( 'NONE', #14288 ) ;
#14657=CLOSED_SHELL ( 'NONE', ( #25407, #23529, #16914, #26676, #28015, #16076, #20160, #3092, #13011, #32238, #3090, #31071, #19527, #11478, #6854, #22610, #28623, #14814, #20317, #13851, #3745, #20639, #22538, #18276, #16512, #23740, #18431, #23338, #25972, #29511, #18766, #11814, #34878, #22051, #8161, #18965, #10367, #10412, #7985, #31937, #20729, #30001, #23777, #14171 ) ) ;
#14705=FACE_OUTER_BOUND ( 'NONE', #662, .T. ) ;
#14717=DIRECTION ( 'NONE',  ( -1.000000000000000000, 5.339440136655842133E-16, 1.047965281155519420E-16 ) ) ;
#14796=DIRECTION ( 'NONE',  ( -1.047965281155519913E-16, -6.938893903907192632E-17, -1.000000000000000000 ) ) ;
#14802=TOROIDAL_SURFACE ( 'NONE', #8487, 6.983999999999990216, 0.04099999999999958539 ) ;
#14805=DIRECTION ( 'NONE',  ( -1.047965281155519790E-16, -6.938893903907192632E-17, -1.000000000000000000 ) ) ;
#14814=ADVANCED_FACE ( 'NONE', ( #15702 ), #29946, .F. ) ;
#14815=DIRECTION ( 'NONE',  ( 1.000000000000000000, -5.339440136655842133E-16, -1.047965281155519420E-16 ) ) ;
#14864=DIRECTION ( 'NONE',  ( 1.000000000000000000, -5.339440136655842133E-16, -1.047965281155519420E-16 ) ) ;
#14885=CARTESIAN_POINT ( 'NONE',  ( -1.479000000000008086, 0.000000000000000000, 0.000000000000000000 ) ) ;
#15015=CARTESIAN_POINT ( 'NONE',  ( -90.00000000000002842, -4.871103520542888323E-16, -7.020000000000039542 ) ) ;
#15025=CARTESIAN_POINT ( 'NONE',  ( -1.519999999999993578, 0.000000000000000000, 0.000000000000000000 ) ) ;
#15118=DIRECTION ( 'NONE',  ( -5.339440136655842133E-16, -1.000000000000000000, 6.938893903907197563E-17 ) ) ;
#15131=AXIS2_PLACEMENT_3D ( 'NONE', #26723, #2060, #4404 ) ;
#15231=DIRECTION ( 'NONE',  ( 1.000000000000000000, -5.339440136655842133E-16, -1.047965281155519420E-16 ) ) ;
#15271=CARTESIAN_POINT ( 'NONE',  ( 1.599999999999990319, 6.765000000000020997, -2.775557561562891351E-14 ) ) ;
#15302=ORIENTED_EDGE ( 'NONE', *, *, #20001, .T. ) ;
#15357=VECTOR ( 'NONE', #18305, 999.9999999999998863 ) ;
#15363=LINE ( 'NONE', #15015, #27628 ) ;
#15376=FACE_OUTER_BOUND ( 'NONE', #25295, .T. ) ;
#15394=ORIENTED_EDGE ( 'NONE', *, *, #23998, .T. ) ;
#15452=VERTEX_POINT ( 'NONE', #32601 ) ;
#15553=EDGE_LOOP ( 'NONE', ( #3791, #28036, #34488, #6651 ) ) ;
#15576=LINE ( 'NONE', #12731, #29454 ) ;
#15577=VERTEX_POINT ( 'NONE', #16564 ) ;
#15589=CIRCLE ( 'NONE', #2426, 8.000000000000051514 ) ;
#15601=EDGE_CURVE ( 'NONE', #2787, #32375, #32634, .T. ) ;
#15658=AXIS2_PLACEMENT_3D ( 'NONE', #15271, #21220, #18520 ) ;
#15702=FACE_OUTER_BOUND ( 'NONE', #33637, .T. ) ;
#15722=DIRECTION ( 'NONE',  ( 1.000000000000000000, -5.339440136655842133E-16, -1.047965281155519420E-16 ) ) ;
#15808=FACE_OUTER_BOUND ( 'NONE', #29078, .T. ) ;
#15856=DIRECTION ( 'NONE',  ( 1.000000000000000000, -5.339440136655842133E-16, -1.047965281155519420E-16 ) ) ;
#15870=CARTESIAN_POINT ( 'NONE',  ( 1.599999999999990319, 0.000000000000000000, 0.000000000000000000 ) ) ;
#15879=CIRCLE ( 'NONE', #29705, 4.000000000000014211 ) ;
#15951=AXIS2_PLACEMENT_3D ( 'NONE', #22732, #14815, #30848 ) ;
#15954=AXIS2_PLACEMENT_3D ( 'NONE', #8037, #24612, #29654 ) ;
#15987=ORIENTED_EDGE ( 'NONE', *, *, #11009, .F. ) ;
#16076=ADVANCED_FACE ( 'NONE', ( #31269 ), #33800, .T. ) ;
#16103=VERTEX_POINT ( 'NONE', #28752 ) ;
#16154=ORIENTED_EDGE ( 'NONE', *, *, #16280, .F. ) ;
#16173=ORIENTED_EDGE ( 'NONE', *, *, #25143, .F. ) ;
#16182=ORIENTED_EDGE ( 'NONE', *, *, #12174, .T. ) ;
#16210=PLANE ( 'NONE',  #6687 ) ;
#16228=DIRECTION ( 'NONE',  ( 1.000000000000000000, -5.339440136655842133E-16, -1.047965281155519420E-16 ) ) ;
#16235=AXIS2_PLACEMENT_3D ( 'NONE', #17718, #1345, #10342 ) ;
#16241=CARTESIAN_POINT ( 'NONE',  ( 1.799999999999996048, 0.000000000000000000, 0.000000000000000000 ) ) ;
#16271=VERTEX_POINT ( 'NONE', #5300 ) ;
#16280=EDGE_CURVE ( 'NONE', #24774, #7064, #2231, .T. ) ;
#16480=FACE_BOUND ( 'NONE', #7881, .T. ) ;
#16487=EDGE_CURVE ( 'NONE', #2787, #21509, #29844, .T. ) ;
#16490=CARTESIAN_POINT ( 'NONE',  ( -2.000000000000001332, -3.278627369596165408E-16, -4.725000000000016520 ) ) ;
#16494=DIRECTION ( 'NONE',  ( 0.000000000000000000, -6.938893903907203726E-17, -1.000000000000000000 ) ) ;
#16512=ADVANCED_FACE ( 'NONE', ( #34070 ), #33274, .T. ) ;
#16513=DIRECTION ( 'NONE',  ( 1.000000000000000000, -5.339440136655842133E-16, -1.047965281155519420E-16 ) ) ;
#16543=DIRECTION ( 'NONE',  ( 1.000000000000000000, -5.339440136655842133E-16, -1.047965281155519420E-16 ) ) ;
#16564=CARTESIAN_POINT ( 'NONE',  ( 1.799999999999996492, -2.775557561562891351E-16, -4.000000000000014211 ) ) ;
#16573=ORIENTED_EDGE ( 'NONE', *, *, #9946, .F. ) ;
#16586=VERTEX_POINT ( 'NONE', #12148 ) ;
#16613=FACE_OUTER_BOUND ( 'NONE', #2154, .T. ) ;
#16639=EDGE_CURVE ( 'NONE', #13171, #3344, #10875, .T. ) ;
#16715=DIRECTION ( 'NONE',  ( 1.000000000000000000, -5.339440136655842133E-16, -1.047965281155519420E-16 ) ) ;
#16739=DIRECTION ( 'NONE',  ( -1.000000000000000000, 5.339440136655842133E-16, 1.047965281155519420E-16 ) ) ;
#16768=VERTEX_POINT ( 'NONE', #7801 ) ;
#16826=CIRCLE ( 'NONE', #4782, 0.04099999999999958539 ) ;
#16884=FACE_OUTER_BOUND ( 'NONE', #29117, .T. ) ;
#16888=CARTESIAN_POINT ( 'NONE',  ( 1.519999999999993578, 0.000000000000000000, 0.000000000000000000 ) ) ;
#16900=EDGE_LOOP ( 'NONE', ( #4972, #7083, #4820, #33974 ) ) ;
#16914=ADVANCED_FACE ( 'NONE', ( #16613 ), #24036, .F. ) ;
#16958=DIRECTION ( 'NONE',  ( 0.000000000000000000, -6.938893903907202493E-17, -1.000000000000000000 ) ) ;
#16995=APPLICATION_CONTEXT ( 'automotive_design' ) ;
#17043=EDGE_LOOP ( 'NONE', ( #35327, #5639 ) ) ;
#17054=DIRECTION ( 'NONE',  ( 1.000000000000000000, -5.339440136655842133E-16, 1.047965281155515476E-16 ) ) ;
#17066=CARTESIAN_POINT ( 'NONE',  ( 1.479000000000008530, -3.480549182199860587E-16, -5.016000000000010672 ) ) ;
#17127=SURFACE_SIDE_STYLE ('',( #25255 ) ) ;
#17168=EDGE_CURVE ( 'NONE', #21050, #23209, #17184, .T. ) ;
#17172=EDGE_LOOP ( 'NONE', ( #23734, #19893 ) ) ;
#17177=CARTESIAN_POINT ( 'NONE',  ( -1.498621416870348888, -3.455569164145799535E-16, -4.980000000000017302 ) ) ;
#17184=CIRCLE ( 'NONE', #35070, 5.016000000000010672 ) ;
#17203=APPLICATION_CONTEXT ( 'automotive_design' ) ;
#17345=TOROIDAL_SURFACE ( 'NONE', #16235, 5.015999999999992909, 0.04099999999999925926 ) ;
#17424=EDGE_CURVE ( 'NONE', #25748, #2812, #32039, .T. ) ;
#17489=DIRECTION ( 'NONE',  ( 5.339440136655842133E-16, 1.000000000000000000, -1.918536189538073087E-16 ) ) ;
#17499=TOROIDAL_SURFACE ( 'NONE', #270, 4.200000000000000178, 0.1999999999999998723 ) ;
#17537=PRODUCT ( 'instrument roller bearing_iso_ISO 1224 - 180816 - R,14,SI,NC,14', 'instrument roller bearing_iso_ISO 1224 - 180816 - R,14,SI,NC,14', '', ( #25346 ) ) ;
#17543=DIRECTION ( 'NONE',  ( -1.047965281155519913E-16, -6.938893903907192632E-17, -1.000000000000000000 ) ) ;
#17564=CARTESIAN_POINT ( 'NONE',  ( 1.799999999999995159, 1.496458227839707357E-15, 7.800000000000051337 ) ) ;
#17667=CONICAL_SURFACE ( 'NONE', #29119, 4.725000000000016520, 0.5675376247847534472 ) ;
#17680=DIRECTION ( 'NONE',  ( 8.645950338799857827E-17, -6.938893903907203726E-17, -1.000000000000000000 ) ) ;
#17682=CIRCLE ( 'NONE', #15954, 8.000000000000049738 ) ;
#17697=EDGE_CURVE ( 'NONE', #16103, #8762, #4019, .T. ) ;
#17718=CARTESIAN_POINT ( 'NONE',  ( -1.479000000000008086, 0.000000000000000000, 0.000000000000000000 ) ) ;
#17720=DIRECTION ( 'NONE',  ( 1.000000000000000000, -5.339440136655842133E-16, -1.047965281155519420E-16 ) ) ;
#17733=CARTESIAN_POINT ( 'NONE',  ( -2.000000000000001776, 0.000000000000000000, 0.000000000000000000 ) ) ;
#17744=CARTESIAN_POINT ( 'NONE',  ( -2.000000000000001332, 1.037758488706469473E-15, 4.724999999999999645 ) ) ;
#17766=DIRECTION ( 'NONE',  ( 1.084202172485500613E-16, -6.938893903907203726E-17, -1.000000000000000000 ) ) ;
#17794=DIRECTION ( 'NONE',  ( 1.000000000000000000, -5.339440136655842133E-16, -1.047965281155519420E-16 ) ) ;
#17821=ORIENTED_EDGE ( 'NONE', *, *, #1841, .F. ) ;
#17834=TOROIDAL_SURFACE ( 'NONE', #11524, 5.015999999999992909, 0.04100000000000673939 ) ;
#17854=EDGE_CURVE ( 'NONE', #33264, #18917, #32631, .T. ) ;
#17895=EDGE_CURVE ( 'NONE', #15452, #23013, #18826, .T. ) ;
#17907=DIRECTION ( 'NONE',  ( 8.645950338799857827E-17, -6.938893903907203726E-17, -1.000000000000000000 ) ) ;
#17911=DIRECTION ( 'NONE',  ( -8.708451184622495809E-17, 6.938893903907203726E-17, 1.000000000000000000 ) ) ;
#17959=ORIENTED_EDGE ( 'NONE', *, *, #12174, .F. ) ;
#18032=CARTESIAN_POINT ( 'NONE',  ( -1.479000000000008086, 0.000000000000000000, 0.000000000000000000 ) ) ;
#18069=DIRECTION ( 'NONE',  ( 1.000000000000000000, -5.339440136655842133E-16, -1.047965281155519420E-16 ) ) ;
#18072=DIRECTION ( 'NONE',  ( -9.266685234918781277E-17, -7.036038418561930364E-15, 1.000000000000000000 ) ) ;
#18093=FACE_OUTER_BOUND ( 'NONE', #33961, .T. ) ;
#18110=CARTESIAN_POINT ( 'NONE',  ( 2.000000000000001776, 0.000000000000000000, 0.000000000000000000 ) ) ;
#18196=AXIS2_PLACEMENT_3D ( 'NONE', #26493, #7869, #18858 ) ;
#18212=VECTOR ( 'NONE', #28126, 1000.000000000000000 ) ;
#18237=ORIENTED_EDGE ( 'NONE', *, *, #26543, .F. ) ;
#18241=EDGE_LOOP ( 'NONE', ( #8895, #26768, #911, #28878 ) ) ;
#18248=ORIENTED_EDGE ( 'NONE', *, *, #17424, .F. ) ;
#18252=DIRECTION ( 'NONE',  ( 1.282131172192753642E-16, -6.938893903907203726E-17, -1.000000000000000000 ) ) ;
#18276=ADVANCED_FACE ( 'NONE', ( #30885 ), #1179, .T. ) ;
#18291=EDGE_CURVE ( 'NONE', #30739, #14603, #21182, .T. ) ;
#18292=DIRECTION ( 'NONE',  ( 1.000000000000000000, 0.000000000000000000, 0.000000000000000000 ) ) ;
#18305=DIRECTION ( 'NONE',  ( 0.8432271980573221581, -3.471037937261304171E-16, 0.5375573387615479870 ) ) ;
#18363=DIRECTION ( 'NONE',  ( 1.000000000000000000, -5.339440136655842133E-16, -1.047965281155519420E-16 ) ) ;
#18406=DIRECTION ( 'NONE',  ( 1.000000000000000000, -5.339440136655842133E-16, -1.047965281155519420E-16 ) ) ;
#18412=VECTOR ( 'NONE', #22740, 999.9999999999998863 ) ;
#18431=ADVANCED_FACE ( 'NONE', ( #35160 ), #30277, .F. ) ;
#18485=DIRECTION ( 'NONE',  ( 1.000000000000000000, -5.339440136655842133E-16, -1.047965281155519420E-16 ) ) ;
#18520=DIRECTION ( 'NONE',  ( -1.047965281155515106E-16, 6.938893903907203726E-17, 1.000000000000000000 ) ) ;
#18584=CARTESIAN_POINT ( 'NONE',  ( 1.599999999999990319, 0.000000000000000000, 0.000000000000000000 ) ) ;
#18710=CARTESIAN_POINT ( 'NONE',  ( -90.00000000000002842, 9.554310223899640008E-16, 4.980000000000024407 ) ) ;
#18716=DIRECTION ( 'NONE',  ( 1.282131172192753642E-16, -6.938893903907203726E-17, -1.000000000000000000 ) ) ;
#18730=EDGE_LOOP ( 'NONE', ( #2751, #25555 ) ) ;
#18740=EDGE_LOOP ( 'NONE', ( #3602, #25781, #4944, #25426 ) ) ;
#18743=AXIS2_PLACEMENT_3D ( 'NONE', #5752, #33460, #3061 ) ;
#18766=ADVANCED_FACE ( 'NONE', ( #26291, #6654 ), #20678, .T. ) ;
#18769=DIRECTION ( 'NONE',  ( 0.000000000000000000, -6.938893903907202493E-17, -1.000000000000000000 ) ) ;
#18778=AXIS2_PLACEMENT_3D ( 'NONE', #29596, #2058, #32287 ) ;
#18780=CIRCLE ( 'NONE', #25708, 4.725000000000016520 ) ;
#18800=AXIS2_PLACEMENT_3D ( 'NONE', #29624, #2443, #2277 ) ;
#18809=VERTEX_POINT ( 'NONE', #25762 ) ;
#18826=CIRCLE ( 'NONE', #3317, 7.020000000000045759 ) ;
#18858=DIRECTION ( 'NONE',  ( 1.000000000000000000, -5.339440136655823397E-16, 0.000000000000000000 ) ) ;
#18875=AXIS2_PLACEMENT_3D ( 'NONE', #16241, #2600, #32832 ) ;
#18900=AXIS2_PLACEMENT_3D ( 'NONE', #32616, #15856, #5267 ) ;
#18917=VERTEX_POINT ( 'NONE', #26654 ) ;
#18935=DIRECTION ( 'NONE',  ( 9.266685234918781277E-17, -6.938893903907202493E-17, -1.000000000000000000 ) ) ;
#18954=VECTOR ( 'NONE', #20644, 1000.000000000000000 ) ;
#18965=ADVANCED_FACE ( 'NONE', ( #15808 ), #10612, .T. ) ;
#19027=DIRECTION ( 'NONE',  ( 0.000000000000000000, -6.938893903907203726E-17, -1.000000000000000000 ) ) ;
#19036=EDGE_LOOP ( 'NONE', ( #34956, #19791, #12281, #5546 ) ) ;
#19040=ORIENTED_EDGE ( 'NONE', *, *, #20535, .T. ) ;
#19088=ORIENTED_EDGE ( 'NONE', *, *, #27956, .T. ) ;
#19116=CARTESIAN_POINT ( 'NONE',  ( -1.498621416870293155, -4.588090364676976828E-14, 7.020000000000020890 ) ) ;
#19169=DIRECTION ( 'NONE',  ( 1.000000000000000000, -5.339440136655842133E-16, -1.047965281155519420E-16 ) ) ;
#19246=AXIS2_PLACEMENT_3D ( 'NONE', #30939, #16543, #30760 ) ;
#19248=VERTEX_POINT ( 'NONE', #2645 ) ;
#19324=DIRECTION ( 'NONE',  ( 5.339440136655842133E-16, 1.000000000000000000, -1.918536189538073087E-16 ) ) ;
#19353=DIRECTION ( 'NONE',  ( 1.000000000000000000, -5.339440136655842133E-16, -1.047965281155519420E-16 ) ) ;
#19376=VERTEX_POINT ( 'NONE', #20221 ) ;
#19458=AXIS2_PLACEMENT_3D ( 'NONE', #7900, #4700, #13152 ) ;
#19505=AXIS2_PLACEMENT_3D ( 'NONE', #6605, #28762, #34166 ) ;
#19527=ADVANCED_FACE ( 'NONE', ( #34523 ), #9840, .F. ) ;
#19550=CARTESIAN_POINT ( 'NONE',  ( 1.599999999999990319, 0.000000000000000000, 0.000000000000000000 ) ) ;
#19583=ORIENTED_EDGE ( 'NONE', *, *, #18291, .F. ) ;
#19613=EDGE_CURVE ( 'NONE', #23209, #21050, #24689, .T. ) ;
#19625=DIRECTION ( 'NONE',  ( 1.000000000000000000, -5.339440136655842133E-16, -1.047965281155519420E-16 ) ) ;
#19674=AXIS2_PLACEMENT_3D ( 'NONE', #34655, #1522, #18252 ) ;
#19754=CARTESIAN_POINT ( 'NONE',  ( -90.00000000000002842, -4.694161725993254197E-16, -6.765000000000038760 ) ) ;
#19774=ADVANCED_BREP_SHAPE_REPRESENTATION ( '', ( #22590, #21307 ), #32842 ) ;
#19782=CARTESIAN_POINT ( 'NONE',  ( 1.479000000000008086, 0.000000000000000000, 0.000000000000000000 ) ) ;
#19791=ORIENTED_EDGE ( 'NONE', *, *, #30883, .T. ) ;
#19828=CARTESIAN_POINT ( 'NONE',  ( -90.00000000000002842, 0.000000000000000000, 6.938893903907228378E-15 ) ) ;
#19871=CONICAL_SURFACE ( 'NONE', #18743, 4.980000000000017302, 0.5675376247847534472 ) ;
#19893=ORIENTED_EDGE ( 'NONE', *, *, #23520, .T. ) ;
#19985=DIRECTION ( 'NONE',  ( 1.000000000000000000, -5.339440136655842133E-16, -1.047965281155519420E-16 ) ) ;
#19997=ORIENTED_EDGE ( 'NONE', *, *, #28678, .T. ) ;
#20001=EDGE_CURVE ( 'NONE', #33264, #16768, #26440, .T. ) ;
#20003=EDGE_CURVE ( 'NONE', #31128, #10764, #5195, .T. ) ;
#20022=ORIENTED_EDGE ( 'NONE', *, *, #11087, .T. ) ;
#20054=EDGE_CURVE ( 'NONE', #23013, #18917, #15363, .T. ) ;
#20110=CARTESIAN_POINT ( 'NONE',  ( 1.599999999999990985, -4.771817072227796402E-14, 6.765000000000020997 ) ) ;
#20118=EDGE_CURVE ( 'NONE', #28617, #25119, #5476, .T. ) ;
#20149=EDGE_LOOP ( 'NONE', ( #29419, #31225 ) ) ;
#20150=CARTESIAN_POINT ( 'NONE',  ( 2.000000000000001776, 0.000000000000000000, 0.000000000000000000 ) ) ;
#20160=ADVANCED_FACE ( 'NONE', ( #7805 ), #2431, .T. ) ;
#20178=CARTESIAN_POINT ( 'NONE',  ( 1.799999999999996048, 0.000000000000000000, 0.000000000000000000 ) ) ;
#20205=ORIENTED_EDGE ( 'NONE', *, *, #17895, .F. ) ;
#20221=CARTESIAN_POINT ( 'NONE',  ( 2.000000000000002665, -4.694161725993254197E-16, -6.765000000000044977 ) ) ;
#20223=FACE_OUTER_BOUND ( 'NONE', #16900, .T. ) ;
#20243=CARTESIAN_POINT ( 'NONE',  ( -1.599999999999990319, 0.000000000000000000, 0.000000000000000000 ) ) ;
#20283=CARTESIAN_POINT ( 'NONE',  ( 1.479000000000008086, 0.000000000000000000, 0.000000000000000000 ) ) ;
#20317=ADVANCED_FACE ( 'NONE', ( #22545 ), #33192, .F. ) ;
#20327=CARTESIAN_POINT ( 'NONE',  ( 1.799999999999996936, -4.652013227827197341E-14, 8.000000000000024869 ) ) ;
#20400=DIRECTION ( 'NONE',  ( 0.000000000000000000, -6.938893903907204958E-17, -1.000000000000000000 ) ) ;
#20411=SURFACE_SIDE_STYLE ('',( #31423 ) ) ;
#20499=CARTESIAN_POINT ( 'NONE',  ( -1.520000000000000906, 9.842294572325847517E-16, 5.016000000000010672 ) ) ;
#20535=EDGE_CURVE ( 'NONE', #4534, #8762, #21300, .T. ) ;
#20573=DIRECTION ( 'NONE',  ( 5.339440136655842133E-16, 1.000000000000000000, -1.918536189538073087E-16 ) ) ;
#20580=EDGE_LOOP ( 'NONE', ( #8620, #7415, #27518, #3599 ) ) ;
#20639=ADVANCED_FACE ( 'NONE', ( #25360, #14705 ), #25718, .T. ) ;
#20644=DIRECTION ( 'NONE',  ( 1.000000000000000000, -5.339440136655842133E-16, -1.047965281155519420E-16 ) ) ;
#20667=CARTESIAN_POINT ( 'NONE',  ( 1.498621416870294487, -4.753539400292362065E-14, 7.020000000000020890 ) ) ;
#20678=PLANE ( 'NONE',  #9672 ) ;
#20702=EDGE_CURVE ( 'NONE', #34245, #25748, #9228, .T. ) ;
#20729=ADVANCED_FACE ( 'NONE', ( #6792 ), #20994, .F. ) ;
#20795=CIRCLE ( 'NONE', #27181, 5.016000000000010672 ) ;
#20803=CARTESIAN_POINT ( 'NONE',  ( -90.00000000000002842, 0.000000000000000000, 6.938893903907228378E-15 ) ) ;
#20901=DIRECTION ( 'NONE',  ( 1.000000000000000000, -5.339440136655842133E-16, -1.047965281155519420E-16 ) ) ;
#20962=ORIENTED_EDGE ( 'NONE', *, *, #22505, .F. ) ;
#20994=CYLINDRICAL_SURFACE ( 'NONE', #1219, 4.000000000000014211 ) ;
#21000=CARTESIAN_POINT ( 'NONE',  ( -2.000000000000000888, -5.412337245047654898E-16, -7.800000000000051337 ) ) ;
#21004=CARTESIAN_POINT ( 'NONE',  ( -1.799999999999996048, 0.000000000000000000, 0.000000000000000000 ) ) ;
#21050=VERTEX_POINT ( 'NONE', #2839 ) ;
#21130=CARTESIAN_POINT ( 'NONE',  ( 1.999999999999999112, -3.982223466972218742E-16, -4.200000000000014388 ) ) ;
#21142=DIRECTION ( 'NONE',  ( 1.000000000000000000, -5.339440136655842133E-16, -1.047965281155519420E-16 ) ) ;
#21149=PRODUCT_DEFINITION ( 'UNKNOWN', '', #33917, #22715 ) ;
#21182=CIRCLE ( 'NONE', #26386, 8.000000000000049738 ) ;
#21184=DIRECTION ( 'NONE',  ( 1.000000000000000000, -5.339440136655842133E-16, -1.047965281155519420E-16 ) ) ;
#21220=DIRECTION ( 'NONE',  ( -1.000000000000000000, 5.339440136655842133E-16, -1.047965281155515476E-16 ) ) ;
#21279=CARTESIAN_POINT ( 'NONE',  ( -2.000000000000001776, 0.000000000000000000, 0.000000000000000000 ) ) ;
#21300=CIRCLE ( 'NONE', #5796, 4.200000000000014388 ) ;
#21301=DIRECTION ( 'NONE',  ( 1.000000000000000000, -5.339440136655842133E-16, -1.047965281155519420E-16 ) ) ;
#21307=AXIS2_PLACEMENT_3D ( 'NONE', #26589, #12725, #18292 ) ;
#21349=DIRECTION ( 'NONE',  ( 1.000000000000000000, -5.339440136655842133E-16, -1.047965281155519420E-16 ) ) ;
#21351=DIRECTION ( 'NONE',  ( 1.000000000000000000, -5.339440136655842133E-16, -1.047965281155519420E-16 ) ) ;
#21376=MECHANICAL_DESIGN_GEOMETRIC_PRESENTATION_REPRESENTATION('',(#4155),#34631);
#21446=CARTESIAN_POINT ( 'NONE',  ( 1.519999999999993578, 5.015999999999978698, 1.387778780781445676E-14 ) ) ;
#21453=DIRECTION ( 'NONE',  ( 1.282131172192753642E-16, -6.938893903907203726E-17, -1.000000000000000000 ) ) ;
#21509=VERTEX_POINT ( 'NONE', #13761 ) ;
#21571=CYLINDRICAL_SURFACE ( 'NONE', #1901, 6.765000000000044977 ) ;
#21578=CARTESIAN_POINT ( 'NONE',  ( 2.000000000000001332, 3.643388353322724362E-16, -4.724999999999999645 ) ) ;
#21602=DIRECTION ( 'NONE',  ( 5.339440136655842133E-16, 1.000000000000000000, -1.918536189538073087E-16 ) ) ;
#21649=TOROIDAL_SURFACE ( 'NONE', #30861, 5.015999999999992909, 0.04100000000000673939 ) ;
#21673=ORIENTED_EDGE ( 'NONE', *, *, #6781, .T. ) ;
#21690=ORIENTED_EDGE ( 'NONE', *, *, #7880, .T. ) ;
#21710=DIRECTION ( 'NONE',  ( 9.266685234918781277E-17, -6.938893903907202493E-17, -1.000000000000000000 ) ) ;
#21735=ORIENTED_EDGE ( 'NONE', *, *, #11535, .F. ) ;
#21745=AXIS2_PLACEMENT_3D ( 'NONE', #11640, #12188, #9126 ) ;
#21788=VERTEX_POINT ( 'NONE', #1677 ) ;
#21815=CARTESIAN_POINT ( 'NONE',  ( -1.498621416870348888, 9.750686088500505778E-16, 4.980000000000000426 ) ) ;
#21824=ORIENTED_EDGE ( 'NONE', *, *, #10023, .F. ) ;
#21861=PLANE ( 'NONE',  #33764 ) ;
#22051=ADVANCED_FACE ( 'NONE', ( #24348, #24527 ), #16210, .T. ) ;
#22139=EDGE_LOOP ( 'NONE', ( #14586, #10091, #8715, #28442 ) ) ;
#22145=ORIENTED_EDGE ( 'NONE', *, *, #9496, .F. ) ;
#22189=AXIS2_PLACEMENT_3D ( 'NONE', #12383, #6977, #24098 ) ;
#22204=CARTESIAN_POINT ( 'NONE',  ( 1.599999999999990319, 0.000000000000000000, 0.000000000000000000 ) ) ;
#22222=ORIENTED_EDGE ( 'NONE', *, *, #27797, .T. ) ;
#22235=AXIS2_PLACEMENT_3D ( 'NONE', #27678, #13978, #19027 ) ;
#22314=CARTESIAN_POINT ( 'NONE',  ( -1.479000000000008086, 0.000000000000000000, 0.000000000000000000 ) ) ;
#22322=ORIENTED_EDGE ( 'NONE', *, *, #23985, .T. ) ;
#22336=AXIS2_PLACEMENT_3D ( 'NONE', #1704, #18069, #29067 ) ;
#22343=DIRECTION ( 'NONE',  ( 1.000000000000000000, -5.339440136655842133E-16, -1.047965281155519420E-16 ) ) ;
#22420=DIRECTION ( 'NONE',  ( 1.000000000000000000, -5.339440136655842133E-16, -1.047965281155519420E-16 ) ) ;
#22457=DIRECTION ( 'NONE',  ( 1.032573497605238773E-16, -6.938893903907203726E-17, -1.000000000000000000 ) ) ;
#22459=FACE_OUTER_BOUND ( 'NONE', #17172, .T. ) ;
#22475=DIRECTION ( 'NONE',  ( -1.047965281155519667E-16, -6.938893903907193865E-17, -1.000000000000000000 ) ) ;
#22503=DIRECTION ( 'NONE',  ( 1.000000000000000000, -5.339440136655842133E-16, -1.047965281155519420E-16 ) ) ;
#22505=EDGE_CURVE ( 'NONE', #34240, #8132, #23178, .T. ) ;
#22510=ORIENTED_EDGE ( 'NONE', *, *, #20118, .T. ) ;
#22538=ADVANCED_FACE ( 'NONE', ( #6227 ), #5863, .T. ) ;
#22545=FACE_OUTER_BOUND ( 'NONE', #8345, .T. ) ;
#22554=DIRECTION ( 'NONE',  ( 9.615983791445651082E-17, -6.938893903907203726E-17, -1.000000000000000000 ) ) ;
#22590=MANIFOLD_SOLID_BREP ( 'InnerRace', #14657 ) ;
#22610=ADVANCED_FACE ( 'NONE', ( #34670 ), #7006, .T. ) ;
#22614=EDGE_CURVE ( 'NONE', #32680, #21788, #20795, .T. ) ;
#22639=ORIENTED_EDGE ( 'NONE', *, *, #431, .F. ) ;
#22649=EDGE_CURVE ( 'NONE', #15452, #11237, #34849, .T. ) ;
#22677=DIRECTION ( 'NONE',  ( 1.112002228190253556E-16, -6.938893903907203726E-17, -1.000000000000000000 ) ) ;
#22715=PRODUCT_DEFINITION_CONTEXT ( 'detailed design', #16995, 'design' ) ;
#22732=CARTESIAN_POINT ( 'NONE',  ( -1.599999999999990319, 0.000000000000000000, 0.000000000000000000 ) ) ;
#22734=DIRECTION ( 'NONE',  ( 1.000000000000000000, -5.339440136655842133E-16, -1.047965281155519420E-16 ) ) ;
#22740=DIRECTION ( 'NONE',  ( -0.8432271980573221581, 4.787673685806302502E-16, -0.5375573387615479870 ) ) ;
#22771=ORIENTED_EDGE ( 'NONE', *, *, #17895, .T. ) ;
#22799=AXIS2_PLACEMENT_3D ( 'NONE', #35353, #16228, #2247 ) ;
#22878=CARTESIAN_POINT ( 'NONE',  ( 1.479000000000008752, -4.846123502488801633E-16, -6.984000000000015085 ) ) ;
#22889=ORIENTED_EDGE ( 'NONE', *, *, #26543, .T. ) ;
#22935=ORIENTED_EDGE ( 'NONE', *, *, #32420, .T. ) ;
#22952=CIRCLE ( 'NONE', #10335, 4.980000000000017302 ) ;
#22965=DIRECTION ( 'NONE',  ( -1.000000000000000000, 5.339440136655842133E-16, 1.047965281155519420E-16 ) ) ;
#22976=DIRECTION ( 'NONE',  ( 5.339440136655842133E-16, 1.000000000000000000, -1.918536189538073087E-16 ) ) ;
#23013=VERTEX_POINT ( 'NONE', #34088 ) ;
#23127=VECTOR ( 'NONE', #22503, 1000.000000000000000 ) ;
#23165=EDGE_CURVE ( 'NONE', #32375, #15577, #12236, .T. ) ;
#23167=ORIENTED_EDGE ( 'NONE', *, *, #23998, .F. ) ;
#23178=CIRCLE ( 'NONE', #10544, 4.980000000000017302 ) ;
#23209=VERTEX_POINT ( 'NONE', #34742 ) ;
#23314=DIRECTION ( 'NONE',  ( 1.000000000000000000, -5.339440136655842133E-16, -1.047965281155519420E-16 ) ) ;
#23338=ADVANCED_FACE ( 'NONE', ( #1977, #29168 ), #34933, .T. ) ;
#23372=ORIENTED_EDGE ( 'NONE', *, *, #22649, .F. ) ;
#23497=PRESENTATION_STYLE_ASSIGNMENT (( #12520 ) ) ;
#23520=EDGE_CURVE ( 'NONE', #5065, #19248, #764, .T. ) ;
#23529=ADVANCED_FACE ( 'NONE', ( #13663 ), #24909, .T. ) ;
#23530=AXIS2_PLACEMENT_3D ( 'NONE', #18584, #13370, #18935 ) ;
#23633=CARTESIAN_POINT ( 'NONE',  ( 1.479000000000008086, 0.000000000000000000, 0.000000000000000000 ) ) ;
#23734=ORIENTED_EDGE ( 'NONE', *, *, #31764, .T. ) ;
#23740=ADVANCED_FACE ( 'NONE', ( #1042, #9314 ), #27703, .T. ) ;
#23748=ORIENTED_EDGE ( 'NONE', *, *, #16487, .F. ) ;
#23777=ADVANCED_FACE ( 'NONE', ( #22459, #33451 ), #8954, .T. ) ;
#23948=CARTESIAN_POINT ( 'NONE',  ( -90.00000000000002842, -4.871103520542888323E-16, -7.020000000000039542 ) ) ;
#23953=AXIS2_PLACEMENT_3D ( 'NONE', #26253, #14717, #1594 ) ;
#23985=EDGE_CURVE ( 'NONE', #3344, #13171, #27819, .T. ) ;
#23989=VERTEX_POINT ( 'NONE', #26429 ) ;
#23998=EDGE_CURVE ( 'NONE', #21509, #15577, #6540, .T. ) ;
#24021=ORIENTED_EDGE ( 'NONE', *, *, #17854, .F. ) ;
#24036=CYLINDRICAL_SURFACE ( 'NONE', #3990, 4.000000000000014211 ) ;
#24047=DIRECTION ( 'NONE',  ( -1.047965281155519667E-16, -6.938893903907192632E-17, -1.000000000000000000 ) ) ;
#24082=EDGE_CURVE ( 'NONE', #14603, #7064, #8337, .T. ) ;
#24090=CARTESIAN_POINT ( 'NONE',  ( 1.799999999999996048, 0.000000000000000000, 0.000000000000000000 ) ) ;
#24098=DIRECTION ( 'NONE',  ( -9.178431089824344374E-17, 6.938893903907203726E-17, 1.000000000000000000 ) ) ;
#24175=DIRECTION ( 'NONE',  ( 1.000000000000000000, -5.339440136655842133E-16, -1.047965281155519420E-16 ) ) ;
#24215=ORIENTED_EDGE ( 'NONE', *, *, #31764, .F. ) ;
#24219=DIRECTION ( 'NONE',  ( 1.000000000000000000, -5.339440136655842133E-16, -1.047965281155519420E-16 ) ) ;
#24256=FACE_OUTER_BOUND ( 'NONE', #29932, .T. ) ;
#24260=TOROIDAL_SURFACE ( 'NONE', #11022, 5.015999999999992909, 0.04099999999999925926 ) ;
#24269=DIRECTION ( 'NONE',  ( 1.084202172485500613E-16, -6.938893903907203726E-17, -1.000000000000000000 ) ) ;
#24348=FACE_OUTER_BOUND ( 'NONE', #17043, .T. ) ;
#24383=CIRCLE ( 'NONE', #3112, 4.980000000000017302 ) ;
#24399=DIRECTION ( 'NONE',  ( 1.000000000000000000, -5.339440136655838189E-16, 0.000000000000000000 ) ) ;
#24491=DIRECTION ( 'NONE',  ( 1.000000000000000000, -5.339440136655842133E-16, -1.047965281155519420E-16 ) ) ;
#24519=CIRCLE ( 'NONE', #4962, 0.04100000000000673939 ) ;
#24527=FACE_BOUND ( 'NONE', #10689, .T. ) ;
#24537=CIRCLE ( 'NONE', #13052, 0.04099999999999958539 ) ;
#24599=AXIS2_PLACEMENT_3D ( 'NONE', #26857, #32775, #7931 ) ;
#24612=DIRECTION ( 'NONE',  ( 1.000000000000000000, -5.339440136655842133E-16, -1.047965281155519420E-16 ) ) ;
#24646=DIRECTION ( 'NONE',  ( -1.047965281155519667E-16, -6.938893903907193865E-17, -1.000000000000000000 ) ) ;
#24658=CARTESIAN_POINT ( 'NONE',  ( -1.799999999999996048, 0.000000000000000000, 0.000000000000000000 ) ) ;
#24689=CIRCLE ( 'NONE', #3441, 5.016000000000010672 ) ;
#24725=VERTEX_POINT ( 'NONE', #1099 ) ;
#24732=VERTEX_POINT ( 'NONE', #33670 ) ;
#24774=VERTEX_POINT ( 'NONE', #20327 ) ;
#24821=MECHANICAL_DESIGN_GEOMETRIC_PRESENTATION_REPRESENTATION('',(#28264),#35194);
#24840=EDGE_CURVE ( 'NONE', #9394, #16271, #1465, .T. ) ;
#24870=LINE ( 'NONE', #14399, #23127 ) ;
#24886=DIRECTION ( 'NONE',  ( 1.000000000000000000, -5.339440136655842133E-16, -1.047965281155519420E-16 ) ) ;
#24897=ORIENTED_EDGE ( 'NONE', *, *, #5148, .F. ) ;
#24909=TOROIDAL_SURFACE ( 'NONE', #8798, 4.200000000000000178, 0.1999999999999998723 ) ;
#24929=EDGE_LOOP ( 'NONE', ( #5900, #25262 ) ) ;
#24971=CARTESIAN_POINT ( 'NONE',  ( -2.000000000000000888, -4.579597227308185762E-14, 6.765000000000020997 ) ) ;
#24986=FACE_OUTER_BOUND ( 'NONE', #30906, .T. ) ;
#24994=DIRECTION ( 'NONE',  ( 1.047965281155515106E-16, -6.938893903907203726E-17, -1.000000000000000000 ) ) ;
#25055=AXIS2_PLACEMENT_3D ( 'NONE', #20150, #909, #22677 ) ;
#25119=VERTEX_POINT ( 'NONE', #27548 ) ;
#25131=FACE_OUTER_BOUND ( 'NONE', #26208, .T. ) ;
#25143=EDGE_CURVE ( 'NONE', #24732, #11716, #350, .T. ) ;
#25213=CARTESIAN_POINT ( 'NONE',  ( 1.498621416870377532, 9.427001662121964880E-16, 4.980000000000000426 ) ) ;
#25219=CYLINDRICAL_SURFACE ( 'NONE', #8105, 7.020000000000045759 ) ;
#25255=SURFACE_STYLE_FILL_AREA ( #8851 ) ;
#25262=ORIENTED_EDGE ( 'NONE', *, *, #15601, .F. ) ;
#25286=VECTOR ( 'NONE', #30632, 1000.000000000000000 ) ;
#25295=EDGE_LOOP ( 'NONE', ( #22639, #5241, #28245, #9398 ) ) ;
#25321=DIRECTION ( 'NONE',  ( 1.000000000000000000, -5.339440136655842133E-16, -1.047965281155519420E-16 ) ) ;
#25329=AXIS2_PLACEMENT_3D ( 'NONE', #29797, #15722, #10517 ) ;
#25346=PRODUCT_CONTEXT ( 'NONE', #17203, 'mechanical' ) ;
#25353=AXIS2_PLACEMENT_3D ( 'NONE', #1050, #33994, #9320 ) ;
#25360=FACE_BOUND ( 'NONE', #33318, .T. ) ;
#25375=DIRECTION ( 'NONE',  ( 1.000000000000000000, -5.339440136655839175E-16, 0.000000000000000000 ) ) ;
#25407=ADVANCED_FACE ( 'NONE', ( #31640 ), #9528, .T. ) ;
#25413=ORIENTED_EDGE ( 'NONE', *, *, #22649, .T. ) ;
#25426=ORIENTED_EDGE ( 'NONE', *, *, #7041, .F. ) ;
#25435=FILL_AREA_STYLE_COLOUR ( '', #8127 ) ;
#25466=DIRECTION ( 'NONE',  ( 8.645950338799857827E-17, -6.938893903907203726E-17, -1.000000000000000000 ) ) ;
#25545=FACE_OUTER_BOUND ( 'NONE', #12393, .T. ) ;
#25555=ORIENTED_EDGE ( 'NONE', *, *, #24840, .T. ) ;
#25646=CIRCLE ( 'NONE', #4399, 0.1999999999999992339 ) ;
#25686=ORIENTED_EDGE ( 'NONE', *, *, #25971, .T. ) ;
#25708=AXIS2_PLACEMENT_3D ( 'NONE', #17733, #23314, #4792 ) ;
#25718=PLANE ( 'NONE',  #25353 ) ;
#25744=ORIENTED_EDGE ( 'NONE', *, *, #24840, .F. ) ;
#25748=VERTEX_POINT ( 'NONE', #16490 ) ;
#25762=CARTESIAN_POINT ( 'NONE',  ( -2.000000000000000888, -4.694161725993254197E-16, -6.765000000000044977 ) ) ;
#25781=ORIENTED_EDGE ( 'NONE', *, *, #435, .T. ) ;
#25883=CONICAL_SURFACE ( 'NONE', #28164, 4.980000000000017302, 0.5675376247847534472 ) ;
#25896=CARTESIAN_POINT ( 'NONE',  ( 1.519999999999994245, -4.846123502488801633E-16, -6.984000000000015085 ) ) ;
#25903=CARTESIAN_POINT ( 'NONE',  ( -1.799999999999995604, 8.399942390771673342E-16, 4.000000000000000000 ) ) ;
#25971=EDGE_CURVE ( 'NONE', #29518, #9746, #14145, .T. ) ;
#25972=ADVANCED_FACE ( 'NONE', ( #15376 ), #12336, .F. ) ;
#25979=EDGE_CURVE ( 'NONE', #25748, #34245, #18780, .T. ) ;
#26034=LINE ( 'NONE', #31431, #13060 ) ;
#26065=AXIS2_PLACEMENT_3D ( 'NONE', #3039, #14001, #24994 ) ;
#26153=AXIS2_PLACEMENT_3D ( 'NONE', #7732, #10628, #18716 ) ;
#26190=DIRECTION ( 'NONE',  ( 1.000000000000000000, -5.339440136655842133E-16, -1.047965281155519420E-16 ) ) ;
#26199=FILL_AREA_STYLE ('',( #28904 ) ) ;
#26208=EDGE_LOOP ( 'NONE', ( #13549, #28313, #29213, #491 ) ) ;
#26220=EDGE_CURVE ( 'NONE', #7064, #16271, #26273, .T. ) ;
#26253=CARTESIAN_POINT ( 'NONE',  ( -1.498621416870349332, 0.000000000000000000, 0.000000000000000000 ) ) ;
#26273=CIRCLE ( 'NONE', #979, 0.2000000000000005107 ) ;
#26291=FACE_BOUND ( 'NONE', #1780, .T. ) ;
#26339=DIRECTION ( 'NONE',  ( -1.047965281155519667E-16, -6.938893903907192632E-17, -1.000000000000000000 ) ) ;
#26386=AXIS2_PLACEMENT_3D ( 'NONE', #34121, #32089, #14478 ) ;
#26429=CARTESIAN_POINT ( 'NONE',  ( 1.599999999999990985, -4.753539400292362697E-14, 7.020000000000020890 ) ) ;
#26440=CIRCLE ( 'NONE', #11489, 6.984000000000015085 ) ;
#26493=CARTESIAN_POINT ( 'NONE',  ( -1.479000000000007642, -3.480549182199860587E-16, -5.016000000000010672 ) ) ;
#26543=EDGE_CURVE ( 'NONE', #28617, #18809, #33595, .T. ) ;
#26544=LINE ( 'NONE', #1877, #18212 ) ;
#26555=CIRCLE ( 'NONE', #5855, 7.020000000000045759 ) ;
#26572=DIRECTION ( 'NONE',  ( 1.000000000000000000, -5.339440136655842133E-16, -1.047965281155519420E-16 ) ) ;
#26589=CARTESIAN_POINT ( 'NONE',  ( 0.000000000000000000, 0.000000000000000000, 0.000000000000000000 ) ) ;
#26595=DIRECTION ( 'NONE',  ( 1.000000000000000000, -5.339440136655842133E-16, -1.047965281155519420E-16 ) ) ;
#26643=ORIENTED_EDGE ( 'NONE', *, *, #34888, .T. ) ;
#26644=AXIS2_PLACEMENT_3D ( 'NONE', #35110, #13315, #11136 ) ;
#26654=CARTESIAN_POINT ( 'NONE',  ( -1.498621416870293155, -4.871103520542888323E-16, -7.020000000000045759 ) ) ;
#26671=AXIS2_PLACEMENT_3D ( 'NONE', #7335, #18485, #17766 ) ;
#26676=ADVANCED_FACE ( 'NONE', ( #30247 ), #17499, .T. ) ;
#26707=EDGE_CURVE ( 'NONE', #18809, #16586, #27726, .T. ) ;
#26717=EDGE_CURVE ( 'NONE', #16271, #9394, #8381, .T. ) ;
#26723=CARTESIAN_POINT ( 'NONE',  ( -1.479000000000008530, 9.623377526722998283E-16, 5.016000000000010672 ) ) ;
#26740=EDGE_CURVE ( 'NONE', #11716, #24732, #27874, .T. ) ;
#26768=ORIENTED_EDGE ( 'NONE', *, *, #5148, .T. ) ;
#26857=CARTESIAN_POINT ( 'NONE',  ( 1.498621416870293821, 0.000000000000000000, 0.000000000000000000 ) ) ;
#26864=DIRECTION ( 'NONE',  ( -1.000000000000000000, 5.339440136655834244E-16, 0.000000000000000000 ) ) ;
#26889=CARTESIAN_POINT ( 'NONE',  ( -1.519999999999993578, 0.000000000000000000, 0.000000000000000000 ) ) ;
#26890=CARTESIAN_POINT ( 'NONE',  ( 1.799999999999996492, -2.914335439641035426E-16, -4.200000000000014388 ) ) ;
#26892=AXIS2_PLACEMENT_3D ( 'NONE', #2310, #35242, #2130 ) ;
#26934=DIRECTION ( 'NONE',  ( 1.000000000000000000, -5.339440136655842133E-16, -1.047965281155519420E-16 ) ) ;
#26972=AXIS2_PLACEMENT_3D ( 'NONE', #1128, #17489, #11924 ) ;
#27060=DIRECTION ( 'NONE',  ( -5.339440136655842133E-16, -1.000000000000000000, 6.938893903907197563E-17 ) ) ;
#27061=DIRECTION ( 'NONE',  ( 8.708451184622495809E-17, -6.938893903907203726E-17, -1.000000000000000000 ) ) ;
#27072=CARTESIAN_POINT ( 'NONE',  ( 1.479000000000008086, 0.000000000000000000, 0.000000000000000000 ) ) ;
#27181=AXIS2_PLACEMENT_3D ( 'NONE', #15025, #6934, #17907 ) ;
#27193=EDGE_LOOP ( 'NONE', ( #1606, #30773, #32010, #25744 ) ) ;
#27240=LINE ( 'NONE', #35347, #5544 ) ;
#27348=DIRECTION ( 'NONE',  ( 1.000000000000000000, -5.339440136655842133E-16, -1.047965281155519420E-16 ) ) ;
#27419=VERTEX_POINT ( 'NONE', #4797 ) ;
#27518=ORIENTED_EDGE ( 'NONE', *, *, #17854, .T. ) ;
#27548=CARTESIAN_POINT ( 'NONE',  ( -1.599999999999989653, -4.579597227308187024E-14, 6.765000000000020997 ) ) ;
#27628=VECTOR ( 'NONE', #17720, 1000.000000000000000 ) ;
#27640=CARTESIAN_POINT ( 'NONE',  ( -90.00000000000002842, 9.554310223899640008E-16, 4.980000000000024407 ) ) ;
#27678=CARTESIAN_POINT ( 'NONE',  ( -90.00000000000002842, 0.000000000000000000, 6.938893903907228378E-15 ) ) ;
#27679=CARTESIAN_POINT ( 'NONE',  ( -90.00000000000002842, 0.000000000000000000, 6.938893903907228378E-15 ) ) ;
#27681=AXIS2_PLACEMENT_3D ( 'NONE', #12442, #15118, #31348 ) ;
#27703=PLANE ( 'NONE',  #26065 ) ;
#27724=ORIENTED_EDGE ( 'NONE', *, *, #26717, .F. ) ;
#27726=LINE ( 'NONE', #19754, #28518 ) ;
#27740=DIRECTION ( 'NONE',  ( 1.000000000000000000, -5.339440136655842133E-16, -1.047965281155519420E-16 ) ) ;
#27741=DIRECTION ( 'NONE',  ( 0.000000000000000000, -6.938893903907202493E-17, -1.000000000000000000 ) ) ;
#27743=EDGE_LOOP ( 'NONE', ( #26643, #33261, #10390, #9529 ) ) ;
#27796=AXIS2_PLACEMENT_3D ( 'NONE', #24658, #25321, #17543 ) ;
#27797=EDGE_CURVE ( 'NONE', #21788, #32680, #14135, .T. ) ;
#27804=CARTESIAN_POINT ( 'NONE',  ( -90.00000000000002842, -5.551115123125799465E-16, -8.000000000000044409 ) ) ;
#27805=AXIS2_PLACEMENT_3D ( 'NONE', #21279, #29408, #21453 ) ;
#27819=CIRCLE ( 'NONE', #13446, 7.800000000000051337 ) ;
#27874=CIRCLE ( 'NONE', #5448, 6.984000000000015085 ) ;
#27892=DIRECTION ( 'NONE',  ( 1.000000000000000000, -5.339440136655842133E-16, -1.047965281155519420E-16 ) ) ;
#27956=EDGE_CURVE ( 'NONE', #3344, #30739, #25646, .T. ) ;
#28004=EDGE_CURVE ( 'NONE', #21050, #9746, #24519, .T. ) ;
#28015=ADVANCED_FACE ( 'NONE', ( #16884 ), #19871, .T. ) ;
#28021=DIRECTION ( 'NONE',  ( 1.000000000000000000, -5.339440136655842133E-16, -1.047965281155519420E-16 ) ) ;
#28026=AXIS2_PLACEMENT_3D ( 'NONE', #24090, #35075, #9676 ) ;
#28036=ORIENTED_EDGE ( 'NONE', *, *, #11009, .T. ) ;
#28107=AXIS2_PLACEMENT_3D ( 'NONE', #8906, #1000, #20400 ) ;
#28114=LINE ( 'NONE', #5967, #25286 ) ;
#28126=DIRECTION ( 'NONE',  ( 1.000000000000000000, -5.339440136655842133E-16, -1.047965281155519420E-16 ) ) ;
#28161=LINE ( 'NONE', #11762, #18412 ) ;
#28164=AXIS2_PLACEMENT_3D ( 'NONE', #20243, #34318, #12166 ) ;
#28245=ORIENTED_EDGE ( 'NONE', *, *, #3733, .T. ) ;
#28264=STYLED_ITEM ( 'NONE', ( #30308 ), #19774 ) ;
#28274=EDGE_CURVE ( 'NONE', #32201, #6784, #10736, .T. ) ;
#28297=DIRECTION ( 'NONE',  ( -1.047965281155519913E-16, -6.938893903907192632E-17, -1.000000000000000000 ) ) ;
#28313=ORIENTED_EDGE ( 'NONE', *, *, #32798, .T. ) ;
#28363=CARTESIAN_POINT ( 'NONE',  ( -1.498621416870349332, 0.000000000000000000, 0.000000000000000000 ) ) ;
#28365=EDGE_CURVE ( 'NONE', #16103, #8708, #15879, .T. ) ;
#28389=TOROIDAL_SURFACE ( 'NONE', #29570, 4.200000000000000178, 0.1999999999999998723 ) ;
#28407=AXIS2_PLACEMENT_3D ( 'NONE', #6632, #34552, #3963 ) ;
#28442=ORIENTED_EDGE ( 'NONE', *, *, #6781, .F. ) ;
#28517=AXIS2_PLACEMENT_3D ( 'NONE', #6767, #14864, #12348 ) ;
#28518=VECTOR ( 'NONE', #14022, 1000.000000000000000 ) ;
#28617=VERTEX_POINT ( 'NONE', #24971 ) ;
#28623=ADVANCED_FACE ( 'NONE', ( #11112 ), #8045, .F. ) ;
#28643=ORIENTED_EDGE ( 'NONE', *, *, #20054, .F. ) ;
#28673=ORIENTED_EDGE ( 'NONE', *, *, #857, .F. ) ;
#28678=EDGE_CURVE ( 'NONE', #19248, #34240, #26034, .T. ) ;
#28752=CARTESIAN_POINT ( 'NONE',  ( -1.799999999999995604, -2.775557561562891351E-16, -4.000000000000014211 ) ) ;
#28762=DIRECTION ( 'NONE',  ( -5.339440136655842133E-16, -1.000000000000000000, 6.938893903907197563E-17 ) ) ;
#28794=AXIS2_PLACEMENT_3D ( 'NONE', #19828, #5825, #16958 ) ;
#28831=ORIENTED_EDGE ( 'NONE', *, *, #7774, .T. ) ;
#28878=ORIENTED_EDGE ( 'NONE', *, *, #34922, .F. ) ;
#28882=TOROIDAL_SURFACE ( 'NONE', #13920, 4.200000000000000178, 0.1999999999999998723 ) ;
#28904=FILL_AREA_STYLE_COLOUR ( '', #3077 ) ;
#28929=AXIS2_PLACEMENT_3D ( 'NONE', #22204, #22734, #22554 ) ;
#29067=DIRECTION ( 'NONE',  ( 1.112002228190253556E-16, -6.938893903907203726E-17, -1.000000000000000000 ) ) ;
#29078=EDGE_LOOP ( 'NONE', ( #11138, #2597, #21673, #34666 ) ) ;
#29085=AXIS2_PLACEMENT_3D ( 'NONE', #12127, #11424, #25466 ) ;
#29117=EDGE_LOOP ( 'NONE', ( #33332, #28831, #17821, #18248 ) ) ;
#29119=AXIS2_PLACEMENT_3D ( 'NONE', #31786, #22965, #7120 ) ;
#29168=FACE_OUTER_BOUND ( 'NONE', #7757, .T. ) ;
#29213=ORIENTED_EDGE ( 'NONE', *, *, #17697, .T. ) ;
#29219=DIRECTION ( 'NONE',  ( 1.000000000000000000, -5.339440136655842133E-16, -1.047965281155519420E-16 ) ) ;
#29231=CARTESIAN_POINT ( 'NONE',  ( 1.498621416870376644, -3.629901386362130586E-16, -4.980000000000000426 ) ) ;
#29238=DIRECTION ( 'NONE',  ( 1.032573497605238773E-16, -6.938893903907203726E-17, -1.000000000000000000 ) ) ;
#29240=DIRECTION ( 'NONE',  ( -1.000000000000000000, 5.339440136655843119E-16, 0.000000000000000000 ) ) ;
#29308=EDGE_CURVE ( 'NONE', #10764, #31128, #11909, .T. ) ;
#29309=CARTESIAN_POINT ( 'NONE',  ( -2.000000000000001776, 0.000000000000000000, 0.000000000000000000 ) ) ;
#29374=AXIS2_PLACEMENT_3D ( 'NONE', #31632, #15231, #12739 ) ;
#29408=DIRECTION ( 'NONE',  ( 1.000000000000000000, -5.339440136655842133E-16, -1.047965281155519420E-16 ) ) ;
#29419=ORIENTED_EDGE ( 'NONE', *, *, #34825, .F. ) ;
#29432=CARTESIAN_POINT ( 'NONE',  ( -90.00000000000002842, 1.297889732222515536E-15, 6.765000000000052083 ) ) ;
#29443=( NAMED_UNIT ( * ) SI_UNIT ( $, .STERADIAN. ) SOLID_ANGLE_UNIT ( ) );
#29447=CARTESIAN_POINT ( 'NONE',  ( -90.00000000000002842, 0.000000000000000000, 6.938893903907228378E-15 ) ) ;
#29454=VECTOR ( 'NONE', #10019, 1000.000000000000000 ) ;
#29476=ORIENTED_EDGE ( 'NONE', *, *, #9946, .T. ) ;
#29501=EDGE_LOOP ( 'NONE', ( #8508, #33135, #12220, #5018 ) ) ;
#29511=ADVANCED_FACE ( 'NONE', ( #8460 ), #7340, .T. ) ;
#29518=VERTEX_POINT ( 'NONE', #25213 ) ;
#29570=AXIS2_PLACEMENT_3D ( 'NONE', #32913, #16513, #13993 ) ;
#29596=CARTESIAN_POINT ( 'NONE',  ( 2.000000000000001776, 0.000000000000000000, 0.000000000000000000 ) ) ;
#29624=CARTESIAN_POINT ( 'NONE',  ( -1.479000000000008752, 1.339905674773393496E-15, 6.984000000000015085 ) ) ;
#29654=DIRECTION ( 'NONE',  ( 1.084202172485497655E-16, -6.938893903907204958E-17, -1.000000000000000000 ) ) ;
#29705=AXIS2_PLACEMENT_3D ( 'NONE', #21004, #2145, #24269 ) ;
#29734=ORIENTED_EDGE ( 'NONE', *, *, #32420, .F. ) ;
#29797=CARTESIAN_POINT ( 'NONE',  ( -90.00000000000002842, 0.000000000000000000, 6.938893903907228378E-15 ) ) ;
#29844=CIRCLE ( 'NONE', #26972, 0.1999999999999998723 ) ;
#29860=EDGE_LOOP ( 'NONE', ( #18237, #22510, #5599, #34341 ) ) ;
#29863=AXIS2_PLACEMENT_3D ( 'NONE', #20803, #10213, #34344 ) ;
#29932=EDGE_LOOP ( 'NONE', ( #8168, #7839 ) ) ;
#29933=VECTOR ( 'NONE', #35198, 1000.000000000000000 ) ;
#29946=CYLINDRICAL_SURFACE ( 'NONE', #3292, 7.020000000000045759 ) ;
#30001=ADVANCED_FACE ( 'NONE', ( #24986 ), #28389, .T. ) ;
#30021=CIRCLE ( 'NONE', #5303, 7.020000000000045759 ) ;
#30043=TOROIDAL_SURFACE ( 'NONE', #12224, 6.983999999999990216, 0.04099999999999958539 ) ;
#30124=ORIENTED_EDGE ( 'NONE', *, *, #20118, .F. ) ;
#30175=ORIENTED_EDGE ( 'NONE', *, *, #19613, .T. ) ;
#30212=EDGE_CURVE ( 'NONE', #24774, #9394, #6054, .T. ) ;
#30247=FACE_OUTER_BOUND ( 'NONE', #19036, .T. ) ;
#30277=CYLINDRICAL_SURFACE ( 'NONE', #18900, 6.765000000000044977 ) ;
#30292=ORIENTED_EDGE ( 'NONE', *, *, #26220, .F. ) ;
#30308=PRESENTATION_STYLE_ASSIGNMENT (( #3477 ) ) ;
#30338=DIRECTION ( 'NONE',  ( -1.000000000000000000, 5.339440136655853966E-16, 0.000000000000000000 ) ) ;
#30382=CYLINDRICAL_SURFACE ( 'NONE', #13796, 4.980000000000017302 ) ;
#30393=VERTEX_POINT ( 'NONE', #2596 ) ;
#30451=CARTESIAN_POINT ( 'NONE',  ( -1.498621416870293821, 0.000000000000000000, 0.000000000000000000 ) ) ;
#30632=DIRECTION ( 'NONE',  ( 1.000000000000000000, -5.339440136655842133E-16, -1.047965281155519420E-16 ) ) ;
#30636=CYLINDRICAL_SURFACE ( 'NONE', #6709, 8.000000000000051514 ) ;
#30654=( NAMED_UNIT ( * ) SI_UNIT ( $, .STERADIAN. ) SOLID_ANGLE_UNIT ( ) );
#30663=AXIS2_PLACEMENT_3D ( 'NONE', #34174, #17054, #30753 ) ;
#30679=CIRCLE ( 'NONE', #15131, 0.04099999999999937028 ) ;
#30724=EDGE_LOOP ( 'NONE', ( #30124, #28673, #35185, #13660 ) ) ;
#30739=VERTEX_POINT ( 'NONE', #4191 ) ;
#30753=DIRECTION ( 'NONE',  ( 1.047965281155515106E-16, -6.938893903907203726E-17, -1.000000000000000000 ) ) ;
#30760=DIRECTION ( 'NONE',  ( 9.615983791445651082E-17, -6.938893903907203726E-17, -1.000000000000000000 ) ) ;
#30770=PRODUCT_DEFINITION_SHAPE ( 'NONE', 'NONE',  #21149 ) ;
#30773=ORIENTED_EDGE ( 'NONE', *, *, #16280, .T. ) ;
#30795=DIRECTION ( 'NONE',  ( 1.000000000000000000, -5.339440136655842133E-16, -1.047965281155519420E-16 ) ) ;
#30832=ORIENTED_EDGE ( 'NONE', *, *, #7041, .T. ) ;
#30848=DIRECTION ( 'NONE',  ( 9.266685234918781277E-17, -6.938893903907202493E-17, -1.000000000000000000 ) ) ;
#30861=AXIS2_PLACEMENT_3D ( 'NONE', #27072, #4762, #2415 ) ;
#30883=EDGE_CURVE ( 'NONE', #8708, #4534, #14393, .T. ) ;
#30885=FACE_OUTER_BOUND ( 'NONE', #13473, .T. ) ;
#30906=EDGE_LOOP ( 'NONE', ( #23748, #8877, #33393, #23167 ) ) ;
#30939=CARTESIAN_POINT ( 'NONE',  ( -1.599999999999990319, 0.000000000000000000, 0.000000000000000000 ) ) ;
#31003=ORIENTED_EDGE ( 'NONE', *, *, #20003, .T. ) ;
#31027=VECTOR ( 'NONE', #1980, 1000.000000000000114 ) ;
#31050=ORIENTED_EDGE ( 'NONE', *, *, #16639, .T. ) ;
#31071=ADVANCED_FACE ( 'NONE', ( #33481 ), #25219, .F. ) ;
#31099=DIRECTION ( 'NONE',  ( -1.000000000000000000, 5.339440136655842133E-16, 1.047965281155519420E-16 ) ) ;
#31114=VECTOR ( 'NONE', #17794, 1000.000000000000000 ) ;
#31128=VERTEX_POINT ( 'NONE', #20667 ) ;
#31155=EDGE_LOOP ( 'NONE', ( #686, #30175, #12091, #32772 ) ) ;
#31176=ORIENTED_EDGE ( 'NONE', *, *, #31215, .T. ) ;
#31215=EDGE_CURVE ( 'NONE', #16103, #15577, #6826, .T. ) ;
#31225=ORIENTED_EDGE ( 'NONE', *, *, #5279, .F. ) ;
#31236=AXIS2_PLACEMENT_3D ( 'NONE', #6026, #19169, #5334 ) ;
#31249=VECTOR ( 'NONE', #14097, 1000.000000000000000 ) ;
#31269=FACE_OUTER_BOUND ( 'NONE', #18241, .T. ) ;
#31274=ORIENTED_EDGE ( 'NONE', *, *, #24082, .F. ) ;
#31348=DIRECTION ( 'NONE',  ( 1.000000000000000000, -5.339440136655843119E-16, 0.000000000000000000 ) ) ;
#31373=FACE_OUTER_BOUND ( 'NONE', #18740, .T. ) ;
#31423=SURFACE_STYLE_FILL_AREA ( #26199 ) ;
#31425=DIRECTION ( 'NONE',  ( -1.000000000000000000, 5.339440136655861854E-16, 0.000000000000000000 ) ) ;
#31430=SHAPE_REPRESENTATION ( 'instrument roller bearing_iso_ISO 1224 - 180816 - R,14,SI,NC,14', ( #21307 ), #32842 ) ;
#31431=CARTESIAN_POINT ( 'NONE',  ( 2.000000000000001332, 3.278627369596165408E-16, 4.725000000000016520 ) ) ;
#31465=DIRECTION ( 'NONE',  ( 1.000000000000000000, -5.339440136655842133E-16, -1.047965281155519420E-16 ) ) ;
#31571=DIRECTION ( 'NONE',  ( 1.000000000000000000, -5.339440136655842133E-16, -1.047965281155519420E-16 ) ) ;
#31632=CARTESIAN_POINT ( 'NONE',  ( -2.000000000000001776, 0.000000000000000000, 0.000000000000000000 ) ) ;
#31640=FACE_OUTER_BOUND ( 'NONE', #15553, .T. ) ;
#31643=EDGE_CURVE ( 'NONE', #18917, #11237, #30021, .T. ) ;
#31716=DIRECTION ( 'NONE',  ( 1.000000000000000000, -5.339440136655842133E-16, -1.047965281155519420E-16 ) ) ;
#31726=CIRCLE ( 'NONE', #8130, 4.725000000000016520 ) ;
#31764=EDGE_CURVE ( 'NONE', #19248, #5065, #31726, .T. ) ;
#31786=CARTESIAN_POINT ( 'NONE',  ( 2.000000000000001776, 0.000000000000000000, 0.000000000000000000 ) ) ;
#31874=CIRCLE ( 'NONE', #28407, 4.980000000000017302 ) ;
#31900=EDGE_CURVE ( 'NONE', #5418, #34867, #15576, .T. ) ;
#31931=EDGE_LOOP ( 'NONE', ( #31050, #19088, #8660, #21735 ) ) ;
#31937=ADVANCED_FACE ( 'NONE', ( #25131 ), #28882, .T. ) ;
#31943=DIRECTION ( 'NONE',  ( 9.314451653655516225E-17, -6.938893903907203726E-17, -1.000000000000000000 ) ) ;
#31997=CARTESIAN_POINT ( 'NONE',  ( -90.00000000000002842, 0.000000000000000000, 6.938893903907228378E-15 ) ) ;
#32010=ORIENTED_EDGE ( 'NONE', *, *, #26220, .T. ) ;
#32039=LINE ( 'NONE', #12955, #31027 ) ;
#32064=CIRCLE ( 'NONE', #28026, 4.000000000000014211 ) ;
#32089=DIRECTION ( 'NONE',  ( 1.000000000000000000, -5.339440136655842133E-16, -1.047965281155519420E-16 ) ) ;
#32201=VERTEX_POINT ( 'NONE', #17177 ) ;
#32238=ADVANCED_FACE ( 'NONE', ( #20223 ), #17345, .T. ) ;
#32287=DIRECTION ( 'NONE',  ( 1.032573497605238773E-16, -6.938893903907203726E-17, -1.000000000000000000 ) ) ;
#32315=ORIENTED_EDGE ( 'NONE', *, *, #11936, .F. ) ;
#32316=DIRECTION ( 'NONE',  ( -5.339440136655842133E-16, -1.000000000000000000, 6.938893903907197563E-17 ) ) ;
#32335=ORIENTED_EDGE ( 'NONE', *, *, #17168, .T. ) ;
#32344=CARTESIAN_POINT ( 'NONE',  ( 1.520000000000021334, 0.000000000000000000, 0.000000000000000000 ) ) ;
#32358=AXIS2_PLACEMENT_3D ( 'NONE', #26890, #27060, #2580 ) ;
#32375=VERTEX_POINT ( 'NONE', #21130 ) ;
#32389=CARTESIAN_POINT ( 'NONE',  ( 1.799999999999996048, 0.000000000000000000, 0.000000000000000000 ) ) ;
#32420=EDGE_CURVE ( 'NONE', #19376, #34867, #11641, .T. ) ;
#32560=EDGE_LOOP ( 'NONE', ( #1727, #10731, #31176, #21690 ) ) ;
#32577=CARTESIAN_POINT ( 'NONE',  ( 1.519999999999993578, 0.000000000000000000, 0.000000000000000000 ) ) ;
#32601=CARTESIAN_POINT ( 'NONE',  ( -1.599999999999989653, -4.588090364676975566E-14, 7.020000000000020890 ) ) ;
#32616=CARTESIAN_POINT ( 'NONE',  ( -90.00000000000002842, 0.000000000000000000, 6.938893903907228378E-15 ) ) ;
#32631=CIRCLE ( 'NONE', #26892, 0.04100000000000673939 ) ;
#32633=ORIENTED_EDGE ( 'NONE', *, *, #32798, .F. ) ;
#32634=CIRCLE ( 'NONE', #997, 4.200000000000014388 ) ;
#32680=VERTEX_POINT ( 'NONE', #20499 ) ;
#32772=ORIENTED_EDGE ( 'NONE', *, *, #25971, .F. ) ;
#32775=DIRECTION ( 'NONE',  ( 1.000000000000000000, -5.339440136655842133E-16, -1.047965281155519420E-16 ) ) ;
#32798=EDGE_CURVE ( 'NONE', #8708, #16103, #9184, .T. ) ;
#32832=DIRECTION ( 'NONE',  ( 1.084202172485497408E-16, -6.938893903907204958E-17, -1.000000000000000000 ) ) ;
#32842=( GEOMETRIC_REPRESENTATION_CONTEXT ( 3 ) GLOBAL_UNCERTAINTY_ASSIGNED_CONTEXT ( ( #5716 ) ) GLOBAL_UNIT_ASSIGNED_CONTEXT ( ( #3302, #33525, #11564 ) ) REPRESENTATION_CONTEXT ( 'NONE', 'WORKASPACE' ) );
#32853=CARTESIAN_POINT ( 'NONE',  ( -1.600000000000018074, 7.019999999999929408, -1.040834085586084257E-14 ) ) ;
#32913=CARTESIAN_POINT ( 'NONE',  ( 1.799999999999996048, 0.000000000000000000, 0.000000000000000000 ) ) ;
#32938=VECTOR ( 'NONE', #24219, 1000.000000000000000 ) ;
#33135=ORIENTED_EDGE ( 'NONE', *, *, #28274, .F. ) ;
#33192=CYLINDRICAL_SURFACE ( 'NONE', #28794, 7.020000000000045759 ) ;
#33218=ORIENTED_EDGE ( 'NONE', *, *, #597, .F. ) ;
#33220=AXIS2_PLACEMENT_3D ( 'NONE', #8210, #3007, #5353 ) ;
#33228=ORIENTED_EDGE ( 'NONE', *, *, #24082, .T. ) ;
#33261=ORIENTED_EDGE ( 'NONE', *, *, #16487, .T. ) ;
#33264=VERTEX_POINT ( 'NONE', #13085 ) ;
#33274=TOROIDAL_SURFACE ( 'NONE', #11427, 7.800000000000023803, 0.2000000000000003164 ) ;
#33297=CARTESIAN_POINT ( 'NONE',  ( 2.000000000000001776, 0.000000000000000000, 0.000000000000000000 ) ) ;
#33318=EDGE_LOOP ( 'NONE', ( #2993, #22889 ) ) ;
#33332=ORIENTED_EDGE ( 'NONE', *, *, #25979, .T. ) ;
#33393=ORIENTED_EDGE ( 'NONE', *, *, #23165, .T. ) ;
#33407=UNCERTAINTY_MEASURE_WITH_UNIT (LENGTH_MEASURE( 1.000000000000000082E-05 ), #4430, 'distance_accuracy_value', 'NONE');
#33451=FACE_BOUND ( 'NONE', #24929, .T. ) ;
#33460=DIRECTION ( 'NONE',  ( 1.000000000000000000, -5.339440136655842133E-16, -1.047965281155519420E-16 ) ) ;
#33481=FACE_OUTER_BOUND ( 'NONE', #2491, .T. ) ;
#33510=CARTESIAN_POINT ( 'NONE',  ( 1.799999999999996048, 0.000000000000000000, 0.000000000000000000 ) ) ;
#33525=( NAMED_UNIT ( * ) PLANE_ANGLE_UNIT ( ) SI_UNIT ( $, .RADIAN. ) );
#33578=DIRECTION ( 'NONE',  ( 8.708451184622495809E-17, -6.938893903907203726E-17, -1.000000000000000000 ) ) ;
#33595=CIRCLE ( 'NONE', #26153, 6.765000000000044977 ) ;
#33637=EDGE_LOOP ( 'NONE', ( #20205, #25413, #1251, #28643 ) ) ;
#33670=CARTESIAN_POINT ( 'NONE',  ( 1.519999999999994245, 1.327174818595651622E-15, 6.983999999999990216 ) ) ;
#33688=ORIENTED_EDGE ( 'NONE', *, *, #3733, .F. ) ;
#33699=( LENGTH_UNIT ( ) NAMED_UNIT ( * ) SI_UNIT ( .MILLI., .METRE. ) );
#33736=CIRCLE ( 'NONE', #22799, 6.765000000000044977 ) ;
#33745=CARTESIAN_POINT ( 'NONE',  ( 1.999999999999998224, 6.989963968728753772E-16, 4.200000000000014388 ) ) ;
#33764=AXIS2_PLACEMENT_3D ( 'NONE', #32853, #8051, #2152 ) ;
#33793=DIRECTION ( 'NONE',  ( 1.000000000000000000, -5.339440136655842133E-16, -1.047965281155519420E-16 ) ) ;
#33800=CYLINDRICAL_SURFACE ( 'NONE', #21745, 4.980000000000017302 ) ;
#33809=ORIENTED_EDGE ( 'NONE', *, *, #31215, .F. ) ;
#33814=CARTESIAN_POINT ( 'NONE',  ( -2.000000000000001776, 0.000000000000000000, 0.000000000000000000 ) ) ;
#33917=PRODUCT_DEFINITION_FORMATION_WITH_SPECIFIED_SOURCE ( 'ANY', '', #17537, .NOT_KNOWN. ) ;
#33961=EDGE_LOOP ( 'NONE', ( #15987, #24215, #19997, #9116 ) ) ;
#33974=ORIENTED_EDGE ( 'NONE', *, *, #7091, .F. ) ;
#33994=DIRECTION ( 'NONE',  ( -1.000000000000000000, 5.339440136655842133E-16, -1.047965281155515476E-16 ) ) ;
#34070=FACE_OUTER_BOUND ( 'NONE', #27193, .T. ) ;
#34088=CARTESIAN_POINT ( 'NONE',  ( -1.599999999999989653, -4.871103520542888323E-16, -7.020000000000045759 ) ) ;
#34121=CARTESIAN_POINT ( 'NONE',  ( -1.799999999999996048, 0.000000000000000000, 0.000000000000000000 ) ) ;
#34126=ORIENTED_EDGE ( 'NONE', *, *, #14308, .F. ) ;
#34152=EDGE_CURVE ( 'NONE', #24725, #5418, #5024, .T. ) ;
#34166=DIRECTION ( 'NONE',  ( 1.000000000000000000, -5.339440136655840161E-16, 0.000000000000000000 ) ) ;
#34174=CARTESIAN_POINT ( 'NONE',  ( 2.000000000000001776, 4.200000000000065015, -2.775557561562891351E-14 ) ) ;
#34179=DIRECTION ( 'NONE',  ( 1.000000000000000000, -5.339440136655842133E-16, -1.047965281155519420E-16 ) ) ;
#34240=VERTEX_POINT ( 'NONE', #34506 ) ;
#34245=VERTEX_POINT ( 'NONE', #17744 ) ;
#34288=AXIS2_PLACEMENT_3D ( 'NONE', #11454, #22420, #17911 ) ;
#34311=CIRCLE ( 'NONE', #18778, 4.200000000000014388 ) ;
#34318=DIRECTION ( 'NONE',  ( 1.000000000000000000, -5.339440136655842133E-16, -1.047965281155519420E-16 ) ) ;
#34319=EDGE_LOOP ( 'NONE', ( #24897, #25686, #7122, #20962 ) ) ;
#34341=ORIENTED_EDGE ( 'NONE', *, *, #26707, .F. ) ;
#34344=DIRECTION ( 'NONE',  ( 0.000000000000000000, -6.938893903907203726E-17, -1.000000000000000000 ) ) ;
#34488=ORIENTED_EDGE ( 'NONE', *, *, #959, .T. ) ;
#34506=CARTESIAN_POINT ( 'NONE',  ( 1.599999999999990763, -4.792677538558942720E-14, 4.980000000000000426 ) ) ;
#34523=FACE_OUTER_BOUND ( 'NONE', #11523, .T. ) ;
#34528=DIRECTION ( 'NONE',  ( 0.000000000000000000, -6.938893903907203726E-17, -1.000000000000000000 ) ) ;
#34552=DIRECTION ( 'NONE',  ( 1.000000000000000000, -5.339440136655842133E-16, -1.047965281155519420E-16 ) ) ;
#34631=( GEOMETRIC_REPRESENTATION_CONTEXT ( 3 ) GLOBAL_UNCERTAINTY_ASSIGNED_CONTEXT ( ( #33407 ) ) GLOBAL_UNIT_ASSIGNED_CONTEXT ( ( #4430, #35038, #29443 ) ) REPRESENTATION_CONTEXT ( 'NONE', 'WORKASPACE' ) );
#34646=ORIENTED_EDGE ( 'NONE', *, *, #20054, .T. ) ;
#34655=CARTESIAN_POINT ( 'NONE',  ( 2.000000000000001776, 0.000000000000000000, 0.000000000000000000 ) ) ;
#34666=ORIENTED_EDGE ( 'NONE', *, *, #28274, .T. ) ;
#34670=FACE_OUTER_BOUND ( 'NONE', #31931, .T. ) ;
#34709=DIRECTION ( 'NONE',  ( 1.112002228190253556E-16, -6.938893903907203726E-17, -1.000000000000000000 ) ) ;
#34742=CARTESIAN_POINT ( 'NONE',  ( 1.520000000000017559, 9.404460481120056357E-16, 5.016000000000010672 ) ) ;
#34750=DIRECTION ( 'NONE',  ( -1.047965281155515106E-16, 6.938893903907203726E-17, 1.000000000000000000 ) ) ;
#34825=EDGE_CURVE ( 'NONE', #16586, #25119, #33736, .T. ) ;
#34849=LINE ( 'NONE', #10174, #14497 ) ;
#34867=VERTEX_POINT ( 'NONE', #2591 ) ;
#34878=ADVANCED_FACE ( 'NONE', ( #7785 ), #21649, .T. ) ;
#34888=EDGE_CURVE ( 'NONE', #32375, #2787, #34311, .T. ) ;
#34921=EDGE_LOOP ( 'NONE', ( #7356, #22322, #13162, #19583 ) ) ;
#34922=EDGE_CURVE ( 'NONE', #9746, #8132, #26544, .T. ) ;
#34933=PLANE ( 'NONE',  #15658 ) ;
#34945=CARTESIAN_POINT ( 'NONE',  ( -90.00000000000002842, 0.000000000000000000, 6.938893903907228378E-15 ) ) ;
#34956=ORIENTED_EDGE ( 'NONE', *, *, #28365, .T. ) ;
#35005=DIRECTION ( 'NONE',  ( 1.000000000000000000, -5.339440136655842133E-16, -1.047965281155519420E-16 ) ) ;
#35024=CARTESIAN_POINT ( 'NONE',  ( -90.00000000000002842, 0.000000000000000000, 6.938893903907228378E-15 ) ) ;
#35038=( NAMED_UNIT ( * ) PLANE_ANGLE_UNIT ( ) SI_UNIT ( $, .RADIAN. ) );
#35070=AXIS2_PLACEMENT_3D ( 'NONE', #9399, #29219, #17680 ) ;
#35075=DIRECTION ( 'NONE',  ( 1.000000000000000000, -5.339440136655842133E-16, -1.047965281155519420E-16 ) ) ;
#35110=CARTESIAN_POINT ( 'NONE',  ( 2.000000000000001776, 0.000000000000000000, 0.000000000000000000 ) ) ;
#35160=FACE_OUTER_BOUND ( 'NONE', #12051, .T. ) ;
#35185=ORIENTED_EDGE ( 'NONE', *, *, #26707, .T. ) ;
#35194=( GEOMETRIC_REPRESENTATION_CONTEXT ( 3 ) GLOBAL_UNCERTAINTY_ASSIGNED_CONTEXT ( ( #35268 ) ) GLOBAL_UNIT_ASSIGNED_CONTEXT ( ( #33699, #9037, #30654 ) ) REPRESENTATION_CONTEXT ( 'NONE', 'WORKASPACE' ) );
#35198=DIRECTION ( 'NONE',  ( 1.000000000000000000, -5.339440136655842133E-16, -1.047965281155519420E-16 ) ) ;
#35242=DIRECTION ( 'NONE',  ( -5.339440136655842133E-16, -1.000000000000000000, 6.938893903907197563E-17 ) ) ;
#35268=UNCERTAINTY_MEASURE_WITH_UNIT (LENGTH_MEASURE( 1.000000000000000082E-05 ), #33699, 'distance_accuracy_value', 'NONE');
#35296=DIRECTION ( 'NONE',  ( 1.000000000000000000, -5.339440136655842133E-16, -1.047965281155519420E-16 ) ) ;
#35327=ORIENTED_EDGE ( 'NONE', *, *, #26740, .T. ) ;
#35347=CARTESIAN_POINT ( 'NONE',  ( -90.00000000000002842, -3.455569164145799535E-16, -4.980000000000010196 ) ) ;
#35353=CARTESIAN_POINT ( 'NONE',  ( -1.599999999999990319, 0.000000000000000000, 0.000000000000000000 ) ) ;
#35355=ORIENTED_EDGE ( 'NONE', *, *, #7774, .F. ) ;
ENDSEC;
END-ISO-10303-21;
